ISO-10303-21;
HEADER;
FILE_DESCRIPTION (('STEP AP214'),
    '1' );
FILE_NAME ('Insert Torx Screw.step',
    '2026-10-09T18:50:44',
    ( '' ),
    ( '' ),
    'SwSTEP 2.0',
    'SolidWorks 2026',
    '' );
FILE_SCHEMA (( 'AUTOMOTIVE_DESIGN' ));
ENDSEC;

DATA;
#73=EDGE_CURVE ( 'NONE', #9964, #7300, #12453, .T. ) ;
#102=EDGE_CURVE ( 'NONE', #7782, #14676, #12670, .T. ) ;
#130=ORIENTED_EDGE ( 'NONE', *, *, #8611, .T. ) ;
#139=DIRECTION ( 'NONE',  ( 0.000000000000000000, 0.1872998510044759646, 0.9823027872370621028 ) ) ;
#144=FACE_OUTER_BOUND ( 'NONE', #9192, .T. ) ;
#146=ORIENTED_EDGE ( 'NONE', *, *, #10088, .T. ) ;
#148=EDGE_LOOP ( 'NONE', ( #12283, #12107, #2323, #5497, #12543, #7117, #9032, #3787, #13140, #10913, #13822, #11755, #4698, #10634, #4086, #13650, #1565 ) ) ;
#223=DIRECTION ( 'NONE',  ( -1.000000000000000000, -1.201369187114119994E-15, -9.616040805000176517E-16 ) ) ;
#245=AXIS2_PLACEMENT_3D ( 'NONE', #11135, #508, #11280 ) ;
#267=EDGE_CURVE ( 'NONE', #7737, #2967, #4813, .T. ) ;
#300=DIRECTION ( 'NONE',  ( 1.000000000000000000, 1.201369187114119994E-15, 9.616040805000176517E-16 ) ) ;
#313=DIRECTION ( 'NONE',  ( 1.000000000000000000, 1.201369187114119994E-15, 9.616040805000176517E-16 ) ) ;
#317=CARTESIAN_POINT ( 'NONE',  ( -14.61203582816999891, -107.9994814593942607, -7.057848339359947154 ) ) ;
#327=ADVANCED_FACE ( 'NONE', ( #7907 ), #7823, .T. ) ;
#335=AXIS2_PLACEMENT_3D ( 'NONE', #317, #9563, #3755 ) ;
#342=DIRECTION ( 'NONE',  ( -1.169602638241521591E-15, 0.1872998510044552312, 0.9823027872370662106 ) ) ;
#356=CARTESIAN_POINT ( 'NONE',  ( -15.61203582816999891, -108.2036686363109084, -6.241690937583108223 ) ) ;
#370=UNCERTAINTY_MEASURE_WITH_UNIT (LENGTH_MEASURE( 1.000000000000000082E-05 ), #958, 'distance_accuracy_value', 'NONE');
#394=EDGE_LOOP ( 'NONE', ( #13412, #6432, #8767, #12041 ) ) ;
#402=CYLINDRICAL_SURFACE ( 'NONE', #9146, 1.249999999999999778 ) ;
#421=VECTOR ( 'NONE', #8848, 1000.000000000000000 ) ;
#422=DIRECTION ( 'NONE',  ( 1.000000000000000275E-15, -0.9823027872370664326, 0.1872998510044542042 ) ) ;
#466=DIRECTION ( 'NONE',  ( 1.000000000000000000, 1.201369187114119994E-15, 9.616040805000176517E-16 ) ) ;
#488=ORIENTED_EDGE ( 'NONE', *, *, #10656, .F. ) ;
#507=DIRECTION ( 'NONE',  ( 1.000000000000000000, 1.201369187114119994E-15, 9.616040805000176517E-16 ) ) ;
#508=DIRECTION ( 'NONE',  ( -1.000000000000000000, -1.201369187114119994E-15, -9.616040805000176517E-16 ) ) ;
#526=CARTESIAN_POINT ( 'NONE',  ( -14.61203582816999891, -107.9151965264422586, -6.615812085103268458 ) ) ;
#531=EDGE_CURVE ( 'NONE', #12074, #14723, #3633, .T. ) ;
#556=AXIS2_PLACEMENT_3D ( 'NONE', #9070, #5629, #975 ) ;
#571=ADVANCED_FACE ( 'NONE', ( #9596, #6439 ), #9749, .F. ) ;
#575=ORIENTED_EDGE ( 'NONE', *, *, #9073, .T. ) ;
#584=CARTESIAN_POINT ( 'NONE',  ( -15.61203582817000068, -106.1207381828630929, -5.933688532728892184 ) ) ;
#611=ORIENTED_EDGE ( 'NONE', *, *, #9222, .F. ) ;
#613=ADVANCED_BREP_SHAPE_REPRESENTATION ( '', ( #7461, #6789 ), #4860 ) ;
#633=VERTEX_POINT ( 'NONE', #356 ) ;
#645=VERTEX_POINT ( 'NONE', #4079 ) ;
#655=CARTESIAN_POINT ( 'NONE',  ( -16.91203582817000139, -106.9280785958314368, -4.859811251109669605 ) ) ;
#718=ORIENTED_EDGE ( 'NONE', *, *, #13711, .T. ) ;
#736=DIRECTION ( 'NONE',  ( 0.000000000000000000, 0.1872998510044495413, 0.9823027872370673208 ) ) ;
#753=DIRECTION ( 'NONE',  ( 1.982541115402064518E-15, -0.1872998510044552312, -0.9823027872370662106 ) ) ;
#760=ORIENTED_EDGE ( 'NONE', *, *, #4717, .T. ) ;
#766=DIRECTION ( 'NONE',  ( 1.000000000000000000, 1.201369187114119994E-15, 9.616040805000176517E-16 ) ) ;
#776=EDGE_LOOP ( 'NONE', ( #8468, #14143, #4177, #7794 ) ) ;
#827=CARTESIAN_POINT ( 'NONE',  ( -15.61203582816999891, -107.1622375242508696, -7.140479451889716778 ) ) ;
#836=FACE_OUTER_BOUND ( 'NONE', #6119, .T. ) ;
#865=SHAPE_REPRESENTATION_RELATIONSHIP ( 'NONE' , 'NONE' ,  #10170, #613 ) ;
#866=EDGE_CURVE ( 'NONE', #8946, #5900, #1818, .T. ) ;
#872=ORIENTED_EDGE ( 'NONE', *, *, #6198, .F. ) ;
#923=VECTOR ( 'NONE', #1746, 1000.000000000000000 ) ;
#952=EDGE_LOOP ( 'NONE', ( #1627, #1662, #4143, #1716 ) ) ;
#958=( LENGTH_UNIT ( ) NAMED_UNIT ( * ) SI_UNIT ( .MILLI., .METRE. ) );
#975=DIRECTION ( 'NONE',  ( 0.000000000000000000, 0.1872998510044759646, 0.9823027872370621028 ) ) ;
#996=DIRECTION ( 'NONE',  ( 0.000000000000000000, 0.1872998510044759646, 0.9823027872370621028 ) ) ;
#1008=DIRECTION ( 'NONE',  ( -1.169602638241521591E-15, 0.1872998510044552312, 0.9823027872370662106 ) ) ;
#1027=ADVANCED_FACE ( 'NONE', ( #4405 ), #7904, .F. ) ;
#1068=CIRCLE ( 'NONE', #11320, 0.9999999999999990008 ) ;
#1072=CARTESIAN_POINT ( 'NONE',  ( -14.61203582816999891, -107.3496051183401647, -7.070526720097523921 ) ) ;
#1092=VERTEX_POINT ( 'NONE', #5912 ) ;
#1094=EDGE_LOOP ( 'NONE', ( #1225, #6586, #13232, #15058 ) ) ;
#1105=DIRECTION ( 'NONE',  ( 0.000000000000000000, 0.1872998510044495413, 0.9823027872370673208 ) ) ;
#1112=DIRECTION ( 'NONE',  ( 0.000000000000000000, 0.1872998510044759646, 0.9823027872370621028 ) ) ;
#1121=EDGE_CURVE ( 'NONE', #9964, #7227, #3529, .T. ) ;
#1144=DIRECTION ( 'NONE',  ( 1.084202172485505026E-15, -0.1872998510044511788, -0.9823027872370668767 ) ) ;
#1151=LINE ( 'NONE', #4836, #1160 ) ;
#1160=VECTOR ( 'NONE', #3603, 1000.000000000000000 ) ;
#1162=EDGE_CURVE ( 'NONE', #12656, #14676, #12577, .T. ) ;
#1198=CARTESIAN_POINT ( 'NONE',  ( -14.61203582817000068, -106.4047424672253186, -6.741402868119605429 ) ) ;
#1224=DIRECTION ( 'NONE',  ( 0.000000000000000000, -0.1872998510044521503, -0.9823027872370667657 ) ) ;
#1225=ORIENTED_EDGE ( 'NONE', *, *, #14950, .T. ) ;
#1264=EDGE_LOOP ( 'NONE', ( #4426, #9254, #14569, #1426 ) ) ;
#1270=CARTESIAN_POINT ( 'NONE',  ( -17.61203582817000424, -106.8344286703292028, -4.368659857491135945 ) ) ;
#1309=CIRCLE ( 'NONE', #335, 0.4500000000000011768 ) ;
#1321=CIRCLE ( 'NONE', #5461, 0.4500000000000011768 ) ;
#1326=CARTESIAN_POINT ( 'NONE',  ( -15.09158957740191731, -107.1622034095870077, -6.087689735156000204 ) ) ;
#1338=AXIS2_PLACEMENT_3D ( 'NONE', #7490, #12099, #1610 ) ;
#1353=CARTESIAN_POINT ( 'NONE',  ( -14.61203582817000068, -107.9196643519486827, -5.433976602192393202 ) ) ;
#1426=ORIENTED_EDGE ( 'NONE', *, *, #3675, .T. ) ;
#1447=EDGE_CURVE ( 'NONE', #7867, #5848, #5803, .T. ) ;
#1471=CARTESIAN_POINT ( 'NONE',  ( -15.61203582817000068, -106.5081018427098201, -6.912624477443467974 ) ) ;
#1488=EDGE_CURVE ( 'NONE', #5098, #9431, #6331, .T. ) ;
#1495=VERTEX_POINT ( 'NONE', #8482 ) ;
#1503=EDGE_CURVE ( 'NONE', #7413, #9431, #12902, .T. ) ;
#1513=CARTESIAN_POINT ( 'NONE',  ( -15.61203582817000068, -106.2504437127206529, -5.561324420954690595 ) ) ;
#1529=CARTESIAN_POINT ( 'NONE',  ( -15.61203582817000068, -106.9748017008338365, -5.104852750214476487 ) ) ;
#1536=VERTEX_POINT ( 'NONE', #6624 ) ;
#1538=PLANE ( 'NONE',  #2993 ) ;
#1553=VERTEX_POINT ( 'NONE', #4428 ) ;
#1565=ORIENTED_EDGE ( 'NONE', *, *, #12915, .F. ) ;
#1583=EDGE_CURVE ( 'NONE', #10777, #12656, #11084, .T. ) ;
#1593=ADVANCED_FACE ( 'NONE', ( #836 ), #7701, .T. ) ;
#1609=VERTEX_POINT ( 'NONE', #11610 ) ;
#1610=DIRECTION ( 'NONE',  ( 0.000000000000000000, 0.1872998510044689147, 0.9823027872370635460 ) ) ;
#1627=ORIENTED_EDGE ( 'NONE', *, *, #6991, .F. ) ;
#1628=CARTESIAN_POINT ( 'NONE',  ( -15.13173615696983276, -107.1622034095870077, -6.087689735156000204 ) ) ;
#1629=CARTESIAN_POINT ( 'NONE',  ( -15.61203582816999891, -106.6563755045979605, -6.855836844165478006 ) ) ;
#1652=AXIS2_PLACEMENT_3D ( 'NONE', #2112, #14959, #10439 ) ;
#1662=ORIENTED_EDGE ( 'NONE', *, *, #14574, .F. ) ;
#1682=CARTESIAN_POINT ( 'NONE',  ( -14.61203582817000246, -105.9033823877427096, -6.327714494218207086 ) ) ;
#1685=DIRECTION ( 'NONE',  ( 0.000000000000000000, -0.1872998510044521503, -0.9823027872370667657 ) ) ;
#1716=ORIENTED_EDGE ( 'NONE', *, *, #3102, .T. ) ;
#1717=DIRECTION ( 'NONE',  ( -1.000000000000000472E-15, 0.9823027872370664326, -0.1872998510044540932 ) ) ;
#1721=VECTOR ( 'NONE', #9876, 1000.000000000000000 ) ;
#1746=DIRECTION ( 'NONE',  ( 0.9635179096299408830, -0.05012965580939084814, -0.2629073133839778253 ) ) ;
#1748=DIRECTION ( 'NONE',  ( 0.7071067811865487940, -0.1324409947604786031, -0.6945929620337749633 ) ) ;
#1758=AXIS2_PLACEMENT_3D ( 'NONE', #6517, #13287, #12127 ) ;
#1814=DIRECTION ( 'NONE',  ( -9.912705577010322591E-16, 0.1872998510044552312, 0.9823027872370662106 ) ) ;
#1818=CIRCLE ( 'NONE', #2057, 0.9999999999999990008 ) ;
#1896=VECTOR ( 'NONE', #5253, 1000.000000000000000 ) ;
#1928=FACE_OUTER_BOUND ( 'NONE', #9172, .T. ) ;
#1929=DIRECTION ( 'NONE',  ( 0.000000000000000000, 0.1872998510044759646, 0.9823027872370621028 ) ) ;
#1949=AXIS2_PLACEMENT_3D ( 'NONE', #11524, #5708, #10378 ) ;
#1963=ADVANCED_FACE ( 'NONE', ( #14808 ), #7762, .T. ) ;
#1966=TOROIDAL_SURFACE ( 'NONE', #5375, 1.600000000000000089, 0.1499999999999999944 ) ;
#1969=ORIENTED_EDGE ( 'NONE', *, *, #4536, .T. ) ;
#1971=EDGE_CURVE ( 'NONE', #14676, #7782, #5575, .T. ) ;
#1981=VERTEX_POINT ( 'NONE', #4033 ) ;
#1984=EDGE_LOOP ( 'NONE', ( #3084, #3204, #2775, #5347 ) ) ;
#1986=DIRECTION ( 'NONE',  ( -9.912705577010322591E-16, 0.1872998510044552312, 0.9823027872370662106 ) ) ;
#1997=ORIENTED_EDGE ( 'NONE', *, *, #12650, .T. ) ;
#2037=ORIENTED_EDGE ( 'NONE', *, *, #7170, .F. ) ;
#2053=ORIENTED_EDGE ( 'NONE', *, *, #12377, .T. ) ;
#2057=AXIS2_PLACEMENT_3D ( 'NONE', #6307, #10987, #5390 ) ;
#2071=COLOUR_RGB ( '', 0.08235294, 0.09019608, 0.10196078) ;
#2085=VECTOR ( 'NONE', #9418, 1000.000000000000000 ) ;
#2107=CIRCLE ( 'NONE', #14801, 1.249999999999999778 ) ;
#2112=CARTESIAN_POINT ( 'NONE',  ( -15.61203582817000068, -106.2173407584721616, -5.758565883178085265 ) ) ;
#2121=DIRECTION ( 'NONE',  ( 0.000000000000000000, 0.1872998510044521503, 0.9823027872370667657 ) ) ;
#2172=AXIS2_PLACEMENT_3D ( 'NONE', #13448, #7613, #13368 ) ;
#2187=AXIS2_PLACEMENT_3D ( 'NONE', #11488, #6880, #13860 ) ;
#2198=DIRECTION ( 'NONE',  ( 1.000000000000000000, 1.201369187114119994E-15, 9.616040805000176517E-16 ) ) ;
#2210=ADVANCED_FACE ( 'NONE', ( #13284 ), #4868, .T. ) ;
#2272=AXIS2_PLACEMENT_3D ( 'NONE', #4471, #9197, #9126 ) ;
#2283=EDGE_LOOP ( 'NONE', ( #5368, #872, #7183, #13927 ) ) ;
#2299=DIRECTION ( 'NONE',  ( 1.000000000000000000, 1.201369187114119994E-15, 9.616040805000176517E-16 ) ) ;
#2304=LINE ( 'NONE', #10555, #11760 ) ;
#2323=ORIENTED_EDGE ( 'NONE', *, *, #6147, .F. ) ;
#2332=FILL_AREA_STYLE_COLOUR ( '', #2071 ) ;
#2337=CARTESIAN_POINT ( 'NONE',  ( -20.61203582816999713, -107.1622034095870077, -6.087689735156005533 ) ) ;
#2344=ORIENTED_EDGE ( 'NONE', *, *, #11055, .T. ) ;
#2345=CARTESIAN_POINT ( 'NONE',  ( -15.61203582817000068, -105.9033823877427096, -6.327714494218207975 ) ) ;
#2348=DIRECTION ( 'NONE',  ( -1.000000000000000000, -1.201369187114119994E-15, -9.616040805000176517E-16 ) ) ;
#2352=DIRECTION ( 'NONE',  ( 1.000000000000000000, 1.201369187114119994E-15, 9.616040805000176517E-16 ) ) ;
#2358=ORIENTED_EDGE ( 'NONE', *, *, #10088, .F. ) ;
#2367=CARTESIAN_POINT ( 'NONE',  ( -20.36203582816999713, -107.1622034095870077, -6.087689735156004645 ) ) ;
#2395=CIRCLE ( 'NONE', #5315, 0.2000000000000012046 ) ;
#2514=CARTESIAN_POINT ( 'NONE',  ( -15.61203582816999891, -107.9196643519486969, -5.433976602192394090 ) ) ;
#2521=ADVANCED_FACE ( 'NONE', ( #13116 ), #9938, .T. ) ;
#2566=CARTESIAN_POINT ( 'NONE',  ( -15.61203582816999713, -107.9994814593942607, -7.057848339359948042 ) ) ;
#2591=ADVANCED_FACE ( 'NONE', ( #4292 ), #4446, .T. ) ;
#2594=DIRECTION ( 'NONE',  ( 0.000000000000000000, 0.1872998510044759646, 0.9823027872370621028 ) ) ;
#2598=ORIENTED_EDGE ( 'NONE', *, *, #14950, .F. ) ;
#2600=DIRECTION ( 'NONE',  ( -1.000000000000000000, -1.201369187114119994E-15, -9.616040805000176517E-16 ) ) ;
#2628=CARTESIAN_POINT ( 'NONE',  ( -16.91203582817000139, -107.3963282233425645, -7.315568219202335243 ) ) ;
#2652=DIRECTION ( 'NONE',  ( -1.000000000000000000, -1.201369187114119994E-15, -9.616040805000176517E-16 ) ) ;
#2676=CARTESIAN_POINT ( 'NONE',  ( -15.61203582817000068, -107.5837463816240529, -4.877506371889844594 ) ) ;
#2683=ORIENTED_EDGE ( 'NONE', *, *, #4717, .F. ) ;
#2685=AXIS2_PLACEMENT_3D ( 'NONE', #10528, #2352, #2121 ) ;
#2693=FACE_OUTER_BOUND ( 'NONE', #11328, .T. ) ;
#2694=EDGE_CURVE ( 'NONE', #11007, #12967, #6281, .T. ) ;
#2710=CARTESIAN_POINT ( 'NONE',  ( -14.61203582817000246, -106.1207381828630929, -5.933688532728891296 ) ) ;
#2717=ORIENTED_EDGE ( 'NONE', *, *, #9636, .T. ) ;
#2743=CARTESIAN_POINT ( 'NONE',  ( -15.61203582817000068, -106.9373417306329515, -4.908392192767062845 ) ) ;
#2773=ORIENTED_EDGE ( 'NONE', *, *, #11870, .F. ) ;
#2775=ORIENTED_EDGE ( 'NONE', *, *, #4775, .F. ) ;
#2776=ORIENTED_EDGE ( 'NONE', *, *, #5519, .F. ) ;
#2782=CYLINDRICAL_SURFACE ( 'NONE', #8299, 0.4500000000000011768 ) ;
#2806=FACE_OUTER_BOUND ( 'NONE', #9597, .T. ) ;
#2818=EDGE_CURVE ( 'NONE', #1609, #11007, #3215, .T. ) ;
#2840=ORIENTED_EDGE ( 'NONE', *, *, #11228, .F. ) ;
#2846=DIRECTION ( 'NONE',  ( -1.000000000000000000, -1.201369187114119994E-15, -9.616040805000176517E-16 ) ) ;
#2849=CARTESIAN_POINT ( 'NONE',  ( -17.61203582817000068, -107.1622034095870077, -6.087689735156001980 ) ) ;
#2857=ORIENTED_EDGE ( 'NONE', *, *, #13842, .F. ) ;
#2869=FACE_OUTER_BOUND ( 'NONE', #8433, .T. ) ;
#2872=VECTOR ( 'NONE', #3243, 1000.000000000000114 ) ;
#2876=AXIS2_PLACEMENT_3D ( 'NONE', #5780, #7148, #11527 ) ;
#2880=EDGE_LOOP ( 'NONE', ( #10500, #9397, #14600, #2776 ) ) ;
#2898=CARTESIAN_POINT ( 'NONE',  ( -15.61203582817000068, -106.2504437127206529, -5.561324420954690595 ) ) ;
#2899=LINE ( 'NONE', #8856, #13519 ) ;
#2907=DIRECTION ( 'NONE',  ( 1.000000000000000000, 1.201369187114119994E-15, 9.616040805000176517E-16 ) ) ;
#2909=AXIS2_PLACEMENT_3D ( 'NONE', #9340, #8186, #13937 ) ;
#2913=LINE ( 'NONE', #3834, #1721 ) ;
#2920=EDGE_CURVE ( 'NONE', #1536, #10256, #15049, .T. ) ;
#2967=VERTEX_POINT ( 'NONE', #11473 ) ;
#2974=ORIENTED_EDGE ( 'NONE', *, *, #12809, .T. ) ;
#2982=CARTESIAN_POINT ( 'NONE',  ( -15.11203582817000246, -106.8344286703292028, -4.368659857491134169 ) ) ;
#2993=AXIS2_PLACEMENT_3D ( 'NONE', #12020, #2907, #12167 ) ;
#3007=AXIS2_PLACEMENT_3D ( 'NONE', #4884, #5104, #12070 ) ;
#3071=CARTESIAN_POINT ( 'NONE',  ( -14.61203582817000246, -106.2173407584721616, -5.758565883178084377 ) ) ;
#3076=CARTESIAN_POINT ( 'NONE',  ( -15.13173615696983276, -106.8354536338428034, -4.374035326349346775 ) ) ;
#3084=ORIENTED_EDGE ( 'NONE', *, *, #12079, .T. ) ;
#3087=ORIENTED_EDGE ( 'NONE', *, *, #102, .T. ) ;
#3095=AXIS2_PLACEMENT_3D ( 'NONE', #9102, #6648, #11331 ) ;
#3102=EDGE_CURVE ( 'NONE', #6974, #8351, #13586, .T. ) ;
#3109=AXIS2_PLACEMENT_3D ( 'NONE', #13229, #6609, #6688 ) ;
#3123=DIRECTION ( 'NONE',  ( -1.169602638241520408E-15, 0.1872998510044540654, 0.9823027872370663216 ) ) ;
#3132=DIRECTION ( 'NONE',  ( 1.000000000000000000, 1.201369187114119994E-15, 9.616040805000176517E-16 ) ) ;
#3157=EDGE_CURVE ( 'NONE', #7867, #9110, #9999, .T. ) ;
#3159=DIRECTION ( 'NONE',  ( 0.000000000000000000, 0.1872998510044759646, 0.9823027872370621028 ) ) ;
#3172=ADVANCED_FACE ( 'NONE', ( #13531 ), #13385, .T. ) ;
#3204=ORIENTED_EDGE ( 'NONE', *, *, #3675, .F. ) ;
#3215=LINE ( 'NONE', #6641, #7710 ) ;
#3243=DIRECTION ( 'NONE',  ( 0.7071067811865471286, 0.1324409947604802129, 0.6945929620337761845 ) ) ;
#3249=ADVANCED_FACE ( 'NONE', ( #5263 ), #4120, .F. ) ;
#3257=CARTESIAN_POINT ( 'NONE',  ( -15.61203582816999891, -108.1070660607018397, -6.416813587133916919 ) ) ;
#3310=( NAMED_UNIT ( * ) SI_UNIT ( $, .STERADIAN. ) SOLID_ANGLE_UNIT ( ) );
#3330=EDGE_LOOP ( 'NONE', ( #10995, #14243, #7000, #3460 ) ) ;
#3360=AXIS2_PLACEMENT_3D ( 'NONE', #6803, #10260, #1008 ) ;
#3365=EDGE_CURVE ( 'NONE', #6540, #10777, #2107, .T. ) ;
#3368=VECTOR ( 'NONE', #313, 1000.000000000000000 ) ;
#3371=CARTESIAN_POINT ( 'NONE',  ( -15.61203582817000068, -106.9748017008338365, -5.104852750214476487 ) ) ;
#3389=CIRCLE ( 'NONE', #3882, 1.249999999999999778 ) ;
#3398=ORIENTED_EDGE ( 'NONE', *, *, #9222, .T. ) ;
#3417=CARTESIAN_POINT ( 'NONE',  ( -15.61203582816999891, -107.8822043817477976, -5.237516044744981336 ) ) ;
#3443=DIRECTION ( 'NONE',  ( 1.000000000000000000, 1.201369187114119994E-15, 9.616040805000176517E-16 ) ) ;
#3460=ORIENTED_EDGE ( 'NONE', *, *, #9073, .F. ) ;
#3470=VERTEX_POINT ( 'NONE', #11990 ) ;
#3475=AXIS2_PLACEMENT_3D ( 'NONE', #2367, #14144, #4737 ) ;
#3480=ORIENTED_EDGE ( 'NONE', *, *, #10083, .F. ) ;
#3510=CIRCLE ( 'NONE', #6673, 0.2000000000000012046 ) ;
#3519=CIRCLE ( 'NONE', #10104, 0.2000000000000012046 ) ;
#3529=CIRCLE ( 'NONE', #6690, 0.1499999999999989397 ) ;
#3532=CONICAL_SURFACE ( 'NONE', #4519, 1.750000000000000666, 0.2709468503384208082 ) ;
#3536=EDGE_CURVE ( 'NONE', #11027, #1495, #14965, .T. ) ;
#3555=DIRECTION ( 'NONE',  ( 0.000000000000000000, -0.1872998510044983078, -0.9823027872370578839 ) ) ;
#3565=EDGE_LOOP ( 'NONE', ( #6068, #8853, #12260, #14273 ) ) ;
#3597=CARTESIAN_POINT ( 'NONE',  ( -14.61203582817000068, -107.1622034095870077, -6.087689735155999315 ) ) ;
#3603=DIRECTION ( 'NONE',  ( 1.000000000000000000, 1.201369187114119994E-15, 9.616040805000176517E-16 ) ) ;
#3626=ADVANCED_FACE ( 'NONE', ( #7339 ), #1538, .F. ) ;
#3633=LINE ( 'NONE', #10746, #9742 ) ;
#3662=CARTESIAN_POINT ( 'NONE',  ( -14.76203582817000104, -107.1622034095870077, -6.087689735155999315 ) ) ;
#3675=EDGE_CURVE ( 'NONE', #633, #8640, #12470, .T. ) ;
#3676=CARTESIAN_POINT ( 'NONE',  ( -14.61203582817000246, -106.9373417306329515, -4.908392192767062845 ) ) ;
#3696=ORIENTED_EDGE ( 'NONE', *, *, #11102, .T. ) ;
#3712=DIRECTION ( 'NONE',  ( 1.000000000000000000, 1.201369187114119994E-15, 9.616040805000176517E-16 ) ) ;
#3722=LINE ( 'NONE', #1270, #10497 ) ;
#3754=ORIENTED_EDGE ( 'NONE', *, *, #1447, .F. ) ;
#3755=DIRECTION ( 'NONE',  ( 0.000000000000000000, 0.1872998510044689147, 0.9823027872370635460 ) ) ;
#3787=ORIENTED_EDGE ( 'NONE', *, *, #7190, .F. ) ;
#3807=AXIS2_PLACEMENT_3D ( 'NONE', #8775, #14974, #4424 ) ;
#3829=DIRECTION ( 'NONE',  ( 1.084202172485505026E-15, -0.1872998510044511788, -0.9823027872370668767 ) ) ;
#3831=EDGE_CURVE ( 'NONE', #11437, #3470, #14472, .T. ) ;
#3834=CARTESIAN_POINT ( 'NONE',  ( -17.61203582816999713, -107.4899781488447985, -7.806719612820868903 ) ) ;
#3837=AXIS2_PLACEMENT_3D ( 'NONE', #1529, #10706, #5954 ) ;
#3846=ORIENTED_EDGE ( 'NONE', *, *, #3157, .T. ) ;
#3848=CARTESIAN_POINT ( 'NONE',  ( -15.61203582816999891, -108.1070660607018397, -6.416813587133916919 ) ) ;
#3857=CARTESIAN_POINT ( 'NONE',  ( -14.61203582816999891, -107.3260907792159031, -6.947204673988433221 ) ) ;
#3873=DIRECTION ( 'NONE',  ( 0.000000000000000000, 0.1872998510044759646, 0.9823027872370621028 ) ) ;
#3882=AXIS2_PLACEMENT_3D ( 'NONE', #9366, #5833, #14264 ) ;
#3886=ORIENTED_EDGE ( 'NONE', *, *, #8276, .T. ) ;
#3893=PRODUCT_DEFINITION_FORMATION_WITH_SPECIFIED_SOURCE ( 'ANY', '', #4461, .NOT_KNOWN. ) ;
#3901=ORIENTED_EDGE ( 'NONE', *, *, #3157, .F. ) ;
#3952=CARTESIAN_POINT ( 'NONE',  ( -14.61203582817000246, -107.1621692949231317, -5.034900018422283630 ) ) ;
#3980=ORIENTED_EDGE ( 'NONE', *, *, #8611, .F. ) ;
#4007=APPLICATION_CONTEXT ( 'automotive_design' ) ;
#4022=AXIS2_PLACEMENT_3D ( 'NONE', #14110, #422, #3555 ) ;
#4023=ADVANCED_FACE ( 'NONE', ( #13438 ), #10981, .F. ) ;
#4032=DIRECTION ( 'NONE',  ( 1.000000000000000000, 1.201369187114119994E-15, 9.616040805000176517E-16 ) ) ;
#4033=CARTESIAN_POINT ( 'NONE',  ( -15.61203582816999891, -107.1622375242508696, -7.140479451889716778 ) ) ;
#4057=AXIS2_PLACEMENT_3D ( 'NONE', #2566, #3712, #7446 ) ;
#4079=CARTESIAN_POINT ( 'NONE',  ( -15.61203582816999891, -107.5495670694337207, -7.066625679870576882 ) ) ;
#4086=ORIENTED_EDGE ( 'NONE', *, *, #12377, .F. ) ;
#4120=CYLINDRICAL_SURFACE ( 'NONE', #3807, 0.2000000000000012046 ) ;
#4123=CARTESIAN_POINT ( 'NONE',  ( -15.11203582816999891, -107.4899781488447985, -7.806719612820867127 ) ) ;
#4132=CIRCLE ( 'NONE', #2909, 0.1500000000000015488 ) ;
#4135=CARTESIAN_POINT ( 'NONE',  ( -14.61203582816999891, -108.1070660607018397, -6.416813587133916030 ) ) ;
#4143=ORIENTED_EDGE ( 'NONE', *, *, #10083, .T. ) ;
#4177=ORIENTED_EDGE ( 'NONE', *, *, #531, .T. ) ;
#4210=AXIS2_PLACEMENT_3D ( 'NONE', #1682, #5201, #6410 ) ;
#4213=ADVANCED_FACE ( 'NONE', ( #8049 ), #5610, .F. ) ;
#4247=DIRECTION ( 'NONE',  ( -9.912705577010322591E-16, 0.1872998510044552312, 0.9823027872370662106 ) ) ;
#4256=DIRECTION ( 'NONE',  ( 0.000000000000000000, 0.1872998510044759646, 0.9823027872370621028 ) ) ;
#4292=FACE_OUTER_BOUND ( 'NONE', #5020, .T. ) ;
#4295=ORIENTED_EDGE ( 'NONE', *, *, #1488, .T. ) ;
#4309=LINE ( 'NONE', #5524, #11058 ) ;
#4323=DIRECTION ( 'NONE',  ( 1.000000000000000000, 1.201369187114119994E-15, 9.616040805000176517E-16 ) ) ;
#4381=CARTESIAN_POINT ( 'NONE',  ( 0.000000000000000000, 0.000000000000000000, 0.000000000000000000 ) ) ;
#4383=VECTOR ( 'NONE', #2198, 1000.000000000000000 ) ;
#4384=EDGE_CURVE ( 'NONE', #12656, #15034, #8616, .T. ) ;
#4391=ORIENTED_EDGE ( 'NONE', *, *, #14773, .F. ) ;
#4398=CIRCLE ( 'NONE', #2685, 1.249999999999999778 ) ;
#4405=FACE_OUTER_BOUND ( 'NONE', #1264, .T. ) ;
#4421=CYLINDRICAL_SURFACE ( 'NONE', #10168, 0.4500000000000011768 ) ;
#4424=DIRECTION ( 'NONE',  ( 0.000000000000000000, 0.1872998510044759646, 0.9823027872370621028 ) ) ;
#4426=ORIENTED_EDGE ( 'NONE', *, *, #7190, .T. ) ;
#4428=CARTESIAN_POINT ( 'NONE',  ( -14.61203582817000068, -108.0739289917894865, -5.561265332623593238 ) ) ;
#4446=CYLINDRICAL_SURFACE ( 'NONE', #3095, 0.4500000000000011768 ) ;
#4452=CIRCLE ( 'NONE', #11298, 0.2000000000000012046 ) ;
#4461=PRODUCT ( 'Insert Torx Screw', 'Insert Torx Screw', '', ( #8569 ) ) ;
#4467=EDGE_LOOP ( 'NONE', ( #12021, #8122, #3087, #5769 ) ) ;
#4471=CARTESIAN_POINT ( 'NONE',  ( -15.61203582817000068, -106.4047424672253186, -6.741402868119606318 ) ) ;
#4483=ORIENTED_EDGE ( 'NONE', *, *, #4384, .T. ) ;
#4519=AXIS2_PLACEMENT_3D ( 'NONE', #11134, #507, #4247 ) ;
#4536=EDGE_CURVE ( 'NONE', #7739, #13230, #4635, .T. ) ;
#4559=DIRECTION ( 'NONE',  ( -1.000000000000000000, -1.201369187114119994E-15, -9.616040805000176517E-16 ) ) ;
#4564=ORIENTED_EDGE ( 'NONE', *, *, #5519, .T. ) ;
#4587=CIRCLE ( 'NONE', #10699, 0.4500000000000011768 ) ;
#4594=AXIS2_PLACEMENT_3D ( 'NONE', #6182, #14307, #7329 ) ;
#4599=ORIENTED_EDGE ( 'NONE', *, *, #10543, .T. ) ;
#4635=CIRCLE ( 'NONE', #2187, 0.2000000000000012046 ) ;
#4640=CARTESIAN_POINT ( 'NONE',  ( -15.61203582817000068, -106.9748017008338365, -5.104852750214476487 ) ) ;
#4677=VERTEX_POINT ( 'NONE', #6037 ) ;
#4685=CIRCLE ( 'NONE', #13244, 0.2000000000000012046 ) ;
#4692=CIRCLE ( 'NONE', #7361, 0.1500000000000015488 ) ;
#4698=ORIENTED_EDGE ( 'NONE', *, *, #11102, .F. ) ;
#4700=ORIENTED_EDGE ( 'NONE', *, *, #12809, .F. ) ;
#4717=EDGE_CURVE ( 'NONE', #15034, #7782, #4132, .T. ) ;
#4737=DIRECTION ( 'NONE',  ( 0.000000000000000000, 0.1872998510044521503, 0.9823027872370667657 ) ) ;
#4747=AXIS2_PLACEMENT_3D ( 'NONE', #7034, #5976, #8268 ) ;
#4760=LINE ( 'NONE', #4838, #2085 ) ;
#4775=EDGE_CURVE ( 'NONE', #5903, #633, #11219, .T. ) ;
#4804=CYLINDRICAL_SURFACE ( 'NONE', #6274, 0.2000000000000012046 ) ;
#4813=LINE ( 'NONE', #9469, #7524 ) ;
#4822=DIRECTION ( 'NONE',  ( 0.000000000000000000, 0.1872998510044759646, 0.9823027872370621028 ) ) ;
#4830=PRODUCT_DEFINITION_CONTEXT ( 'detailed design', #10258, 'design' ) ;
#4833=CARTESIAN_POINT ( 'NONE',  ( -14.61203582816999891, -108.4210244314312916, -5.847664976093791545 ) ) ;
#4836=CARTESIAN_POINT ( 'NONE',  ( -15.61203582817000068, -106.1207381828630929, -5.933688532728892184 ) ) ;
#4838=CARTESIAN_POINT ( 'NONE',  ( -15.61203582816999891, -107.8822043817477976, -5.237516044744980448 ) ) ;
#4841=CIRCLE ( 'NONE', #1652, 0.2000000000000012046 ) ;
#4860=( GEOMETRIC_REPRESENTATION_CONTEXT ( 3 ) GLOBAL_UNCERTAINTY_ASSIGNED_CONTEXT ( ( #13661 ) ) GLOBAL_UNIT_ASSIGNED_CONTEXT ( ( #14710, #8891, #3310 ) ) REPRESENTATION_CONTEXT ( 'NONE', 'WORKASPACE' ) );
#4868=CYLINDRICAL_SURFACE ( 'NONE', #4057, 0.4500000000000011768 ) ;
#4870=EDGE_CURVE ( 'NONE', #7946, #12967, #13836, .T. ) ;
#4884=CARTESIAN_POINT ( 'NONE',  ( -15.61203582817000068, -107.5837463816240529, -4.877506371889844594 ) ) ;
#4899=CARTESIAN_POINT ( 'NONE',  ( -14.61203582816999891, -107.4618831711941169, -7.659374194735305785 ) ) ;
#4927=ORIENTED_EDGE ( 'NONE', *, *, #10780, .T. ) ;
#4948=CIRCLE ( 'NONE', #9077, 0.2000000000000012046 ) ;
#4991=FACE_OUTER_BOUND ( 'NONE', #3330, .T. ) ;
#5015=CARTESIAN_POINT ( 'NONE',  ( -15.61203582816999713, -107.9994814593942607, -7.057848339359948042 ) ) ;
#5020=EDGE_LOOP ( 'NONE', ( #13892, #9003, #10636, #6944 ) ) ;
#5060=CIRCLE ( 'NONE', #13367, 0.2000000000000012046 ) ;
#5079=DIRECTION ( 'NONE',  ( 9.943800201373337757E-16, -0.1872998510044509290, -0.9823027872370669877 ) ) ;
#5098=VERTEX_POINT ( 'NONE', #1513 ) ;
#5104=DIRECTION ( 'NONE',  ( 1.000000000000000000, 1.201369187114119994E-15, 9.616040805000176517E-16 ) ) ;
#5106=FACE_OUTER_BOUND ( 'NONE', #8625, .T. ) ;
#5124=DIRECTION ( 'NONE',  ( -9.912705577010322591E-16, 0.1872998510044552312, 0.9823027872370662106 ) ) ;
#5134=DIRECTION ( 'NONE',  ( 0.9635179096299403279, 0.05012965580939313798, 0.2629073133839797682 ) ) ;
#5140=DIRECTION ( 'NONE',  ( 0.000000000000000000, 0.1872998510044689147, 0.9823027872370635460 ) ) ;
#5180=CARTESIAN_POINT ( 'NONE',  ( -15.61203582817000068, -106.9748017008338365, -5.104852750214476487 ) ) ;
#5181=CONICAL_SURFACE ( 'NONE', #11770, 1.750000000000000666, 0.2709468503384208082 ) ;
#5186=VECTOR ( 'NONE', #3132, 1000.000000000000000 ) ;
#5201=DIRECTION ( 'NONE',  ( 1.000000000000000000, 1.201369187114119994E-15, 9.616040805000176517E-16 ) ) ;
#5216=AXIS2_PLACEMENT_3D ( 'NONE', #12293, #8832, #1814 ) ;
#5225=CIRCLE ( 'NONE', #11326, 1.750000000000000666 ) ;
#5253=DIRECTION ( 'NONE',  ( 1.000000000000000000, 1.201369187114119994E-15, 9.616040805000176517E-16 ) ) ;
#5263=FACE_OUTER_BOUND ( 'NONE', #8023, .T. ) ;
#5315=AXIS2_PLACEMENT_3D ( 'NONE', #1353, #10456, #15118 ) ;
#5347=ORIENTED_EDGE ( 'NONE', *, *, #13842, .T. ) ;
#5365=DIRECTION ( 'NONE',  ( 1.000000000000000000, 1.201369187114119994E-15, 9.616040805000176517E-16 ) ) ;
#5368=ORIENTED_EDGE ( 'NONE', *, *, #3536, .F. ) ;
#5375=AXIS2_PLACEMENT_3D ( 'NONE', #9514, #14184, #13125 ) ;
#5390=DIRECTION ( 'NONE',  ( 0.000000000000000000, 0.1872998510044495413, 0.9823027872370673208 ) ) ;
#5414=CARTESIAN_POINT ( 'NONE',  ( -15.61203582817000068, -107.1622034095870077, -6.087689735156000204 ) ) ;
#5447=AXIS2_PLACEMENT_3D ( 'NONE', #8328, #10709, #1224 ) ;
#5461=AXIS2_PLACEMENT_3D ( 'NONE', #6169, #223, #8240 ) ;
#5464=LINE ( 'NONE', #15025, #6826 ) ;
#5467=AXIS2_PLACEMENT_3D ( 'NONE', #13968, #2348, #11670 ) ;
#5479=CARTESIAN_POINT ( 'NONE',  ( -15.61203582817000068, -106.2173407584721616, -5.758565883178085265 ) ) ;
#5488=CARTESIAN_POINT ( 'NONE',  ( -14.61203582817000068, -107.9196643519486827, -5.433976602192393202 ) ) ;
#5497=ORIENTED_EDGE ( 'NONE', *, *, #14487, .F. ) ;
#5519=EDGE_CURVE ( 'NONE', #7300, #4677, #4692, .T. ) ;
#5524=CARTESIAN_POINT ( 'NONE',  ( -15.61203582817000068, -106.2504778273845147, -6.614114137688407169 ) ) ;
#5535=( NAMED_UNIT ( * ) SI_UNIT ( $, .STERADIAN. ) SOLID_ANGLE_UNIT ( ) );
#5548=CARTESIAN_POINT ( 'NONE',  ( -14.61203582816999891, -107.1622375242508696, -7.140479451889715889 ) ) ;
#5575=CIRCLE ( 'NONE', #5216, 1.750000000000000666 ) ;
#5576=DIRECTION ( 'NONE',  ( 1.000000000000000000, 1.201369187114119994E-15, 9.616040805000176517E-16 ) ) ;
#5579=EDGE_CURVE ( 'NONE', #1981, #7737, #14700, .T. ) ;
#5608=ORIENTED_EDGE ( 'NONE', *, *, #13711, .F. ) ;
#5610=CYLINDRICAL_SURFACE ( 'NONE', #2272, 0.2000000000000012046 ) ;
#5629=DIRECTION ( 'NONE',  ( 1.000000000000000000, 1.201369187114119994E-15, 9.616040805000176517E-16 ) ) ;
#5643=ORIENTED_EDGE ( 'NONE', *, *, #1162, .T. ) ;
#5644=CIRCLE ( 'NONE', #9557, 0.4500000000000011768 ) ;
#5649=EDGE_CURVE ( 'NONE', #14723, #11853, #4948, .T. ) ;
#5651=CIRCLE ( 'NONE', #6864, 1.599999999999999201 ) ;
#5683=ORIENTED_EDGE ( 'NONE', *, *, #1162, .F. ) ;
#5687=SURFACE_STYLE_USAGE ( .BOTH. , #10122 ) ;
#5697=ORIENTED_EDGE ( 'NONE', *, *, #6289, .T. ) ;
#5700=DIRECTION ( 'NONE',  ( -1.000000000000000000, -1.201369187114119994E-15, -9.616040805000176517E-16 ) ) ;
#5708=DIRECTION ( 'NONE',  ( -1.000000000000000000, -1.201369187114119994E-15, -9.616040805000176517E-16 ) ) ;
#5743=CARTESIAN_POINT ( 'NONE',  ( -14.61203582817000068, -106.7406604375499626, -7.297873098422155813 ) ) ;
#5769=ORIENTED_EDGE ( 'NONE', *, *, #8102, .F. ) ;
#5779=DIRECTION ( 'NONE',  ( 0.000000000000000000, 0.1872998510044759646, 0.9823027872370621028 ) ) ;
#5780=CARTESIAN_POINT ( 'NONE',  ( -15.61203582817000246, -106.3249253597797406, -5.117531130952053253 ) ) ;
#5796=CONICAL_SURFACE ( 'NONE', #9715, 0.9999999999999990008, 0.7853981633974476129 ) ;
#5800=CARTESIAN_POINT ( 'NONE',  ( -14.61203582817000068, -107.8822043817477976, -5.237516044744977783 ) ) ;
#5803=CIRCLE ( 'NONE', #13636, 0.4500000000000011768 ) ;
#5806=FACE_OUTER_BOUND ( 'NONE', #1094, .T. ) ;
#5819=CARTESIAN_POINT ( 'NONE',  ( -15.61203582817000068, -107.1621692949231459, -5.034900018422284518 ) ) ;
#5833=DIRECTION ( 'NONE',  ( -1.000000000000000000, -1.201369187114119994E-15, -9.616040805000176517E-16 ) ) ;
#5843=AXIS2_PLACEMENT_3D ( 'NONE', #10762, #12065, #3873 ) ;
#5848=VERTEX_POINT ( 'NONE', #6284 ) ;
#5900=VERTEX_POINT ( 'NONE', #12261 ) ;
#5903=VERTEX_POINT ( 'NONE', #7507 ) ;
#5912=CARTESIAN_POINT ( 'NONE',  ( -14.61203582817000068, -106.5081018427098201, -6.912624477443467974 ) ) ;
#5943=EDGE_CURVE ( 'NONE', #7946, #645, #12758, .T. ) ;
#5954=DIRECTION ( 'NONE',  ( 0.000000000000000000, 0.1872998510044759646, 0.9823027872370621028 ) ) ;
#5976=DIRECTION ( 'NONE',  ( -1.000000000000000000, -1.201369187114119994E-15, -9.616040805000176517E-16 ) ) ;
#5990=DIRECTION ( 'NONE',  ( 0.000000000000000000, 0.1872998510044689147, 0.9823027872370635460 ) ) ;
#6003=DIRECTION ( 'NONE',  ( 1.000000000000000000, 1.201369187114119994E-15, 9.616040805000176517E-16 ) ) ;
#6013=DIRECTION ( 'NONE',  ( 9.912705577010322591E-16, -0.1872998510044552312, -0.9823027872370662106 ) ) ;
#6020=ADVANCED_FACE ( 'NONE', ( #1928 ), #13627, .T. ) ;
#6024=DIRECTION ( 'NONE',  ( 0.000000000000000000, 0.1872998510044689147, 0.9823027872370635460 ) ) ;
#6034=CIRCLE ( 'NONE', #8974, 0.2000000000000012046 ) ;
#6037=CARTESIAN_POINT ( 'NONE',  ( -14.76203582816999926, -107.4899781488447985, -7.806719612820866239 ) ) ;
#6039=CARTESIAN_POINT ( 'NONE',  ( -15.61203582816999713, -107.9151965264422586, -6.615812085103269347 ) ) ;
#6068=ORIENTED_EDGE ( 'NONE', *, *, #4870, .F. ) ;
#6102=ORIENTED_EDGE ( 'NONE', *, *, #73, .T. ) ;
#6117=DIRECTION ( 'NONE',  ( 1.000000000000000000, 1.201369187114119994E-15, 9.616040805000176517E-16 ) ) ;
#6119=EDGE_LOOP ( 'NONE', ( #11961, #1997, #3398, #13963, #4599, #130, #12350, #9737, #9565, #10862, #4927, #2344, #12671, #3886, #12123, #2974, #1969 ) ) ;
#6120=CARTESIAN_POINT ( 'NONE',  ( -15.61203582816999891, -108.4210244314312916, -5.847664976093792433 ) ) ;
#6126=DIRECTION ( 'NONE',  ( 1.000000000000000000, 1.201369187114119994E-15, 9.616040805000176517E-16 ) ) ;
#6147=EDGE_CURVE ( 'NONE', #2967, #1092, #4587, .T. ) ;
#6169=CARTESIAN_POINT ( 'NONE',  ( -14.61203582817000246, -106.3249253597797406, -5.117531130952052365 ) ) ;
#6182=CARTESIAN_POINT ( 'NONE',  ( -14.61203582817000246, -106.2173407584721616, -5.758565883178084377 ) ) ;
#6192=FACE_OUTER_BOUND ( 'NONE', #11819, .T. ) ;
#6198=EDGE_CURVE ( 'NONE', #6401, #11027, #1151, .T. ) ;
#6274=AXIS2_PLACEMENT_3D ( 'NONE', #12365, #8912, #4256 ) ;
#6281=CIRCLE ( 'NONE', #3109, 0.4500000000000011768 ) ;
#6284=CARTESIAN_POINT ( 'NONE',  ( -15.61203582817000068, -107.8163049764641812, -5.262754992868533321 ) ) ;
#6289=EDGE_CURVE ( 'NONE', #1092, #1495, #6034, .T. ) ;
#6307=CARTESIAN_POINT ( 'NONE',  ( -20.61203582816999713, -107.1622034095870077, -6.087689735156005533 ) ) ;
#6331=LINE ( 'NONE', #2898, #3368 ) ;
#6340=EDGE_CURVE ( 'NONE', #5098, #12074, #12402, .T. ) ;
#6341=EDGE_CURVE ( 'NONE', #8351, #1553, #2395, .T. ) ;
#6369=DIRECTION ( 'NONE',  ( 0.000000000000000000, 0.1872998510044983078, 0.9823027872370578839 ) ) ;
#6396=AXIS2_PLACEMENT_3D ( 'NONE', #12206, #12431, #7236 ) ;
#6401=VERTEX_POINT ( 'NONE', #584 ) ;
#6410=DIRECTION ( 'NONE',  ( 0.000000000000000000, 0.1872998510044689147, 0.9823027872370635460 ) ) ;
#6415=DIRECTION ( 'NONE',  ( -1.000000000000000000, -1.201369187114119994E-15, -9.616040805000176517E-16 ) ) ;
#6432=ORIENTED_EDGE ( 'NONE', *, *, #12455, .T. ) ;
#6439=FACE_OUTER_BOUND ( 'NONE', #10620, .T. ) ;
#6505=CARTESIAN_POINT ( 'NONE',  ( -15.61203582817000068, -106.5081018427098201, -6.912624477443467974 ) ) ;
#6517=CARTESIAN_POINT ( 'NONE',  ( -15.61203582816999891, -106.7406604375499626, -7.297873098422156701 ) ) ;
#6540=VERTEX_POINT ( 'NONE', #655 ) ;
#6549=DIRECTION ( 'NONE',  ( -1.000000000000000000, -1.201369187114119994E-15, -9.616040805000176517E-16 ) ) ;
#6554=EDGE_LOOP ( 'NONE', ( #2053, #15105, #10332, #4295 ) ) ;
#6562=LINE ( 'NONE', #12320, #8843 ) ;
#6586=ORIENTED_EDGE ( 'NONE', *, *, #8553, .T. ) ;
#6609=DIRECTION ( 'NONE',  ( -1.000000000000000000, -1.201369187114119994E-15, -9.616040805000176517E-16 ) ) ;
#6618=DIRECTION ( 'NONE',  ( 1.000000000000000000, 1.201369187114119994E-15, 9.616040805000176517E-16 ) ) ;
#6624=CARTESIAN_POINT ( 'NONE',  ( -14.61203582816999891, -107.5495670694337207, -7.066625679870575105 ) ) ;
#6641=CARTESIAN_POINT ( 'NONE',  ( -15.61203582816999713, -108.0739631064533484, -6.614055049357310700 ) ) ;
#6643=CYLINDRICAL_SURFACE ( 'NONE', #9606, 0.2000000000000012046 ) ;
#6648=DIRECTION ( 'NONE',  ( 1.000000000000000000, 1.201369187114119994E-15, 9.616040805000176517E-16 ) ) ;
#6664=ORIENTED_EDGE ( 'NONE', *, *, #3365, .T. ) ;
#6673=AXIS2_PLACEMENT_3D ( 'NONE', #5479, #8992, #13745 ) ;
#6688=DIRECTION ( 'NONE',  ( 0.000000000000000000, 0.1872998510044689147, 0.9823027872370635460 ) ) ;
#6690=AXIS2_PLACEMENT_3D ( 'NONE', #7134, #14267, #12049 ) ;
#6693=AXIS2_PLACEMENT_3D ( 'NONE', #4135, #8791, #10948 ) ;
#6718=CARTESIAN_POINT ( 'NONE',  ( -14.61203582817000246, -106.8625236479798843, -4.516005275576693734 ) ) ;
#6736=LINE ( 'NONE', #10421, #2872 ) ;
#6761=CARTESIAN_POINT ( 'NONE',  ( -15.13173615696983099, -107.4889531853311979, -7.801344143962656297 ) ) ;
#6789=AXIS2_PLACEMENT_3D ( 'NONE', #4381, #12419, #6809 ) ;
#6790=CARTESIAN_POINT ( 'NONE',  ( -15.61203582816999891, -107.3496051183401647, -7.070526720097524809 ) ) ;
#6803=CARTESIAN_POINT ( 'NONE',  ( -15.09158957740191731, -107.1622034095870077, -6.087689735156000204 ) ) ;
#6809=DIRECTION ( 'NONE',  ( 1.000000000000000000, 0.000000000000000000, 0.000000000000000000 ) ) ;
#6826=VECTOR ( 'NONE', #4323, 1000.000000000000000 ) ;
#6845=CARTESIAN_POINT ( 'NONE',  ( -15.61203582817000068, -106.2173407584721616, -5.758565883178085265 ) ) ;
#6864=AXIS2_PLACEMENT_3D ( 'NONE', #3597, #3443, #1144 ) ;
#6870=CARTESIAN_POINT ( 'NONE',  ( -15.61203582817000068, -106.9373417306329515, -4.908392192767063733 ) ) ;
#6880=DIRECTION ( 'NONE',  ( 1.000000000000000000, 1.201369187114119994E-15, 9.616040805000176517E-16 ) ) ;
#6911=CYLINDRICAL_SURFACE ( 'NONE', #7860, 0.2000000000000012046 ) ;
#6941=DIRECTION ( 'NONE',  ( 1.000000000000000000, 1.201369187114119994E-15, 9.616040805000176517E-16 ) ) ;
#6944=ORIENTED_EDGE ( 'NONE', *, *, #14487, .T. ) ;
#6955=DIRECTION ( 'NONE',  ( 1.000000000000000000, 1.201369187114119994E-15, 9.616040805000176517E-16 ) ) ;
#6974=VERTEX_POINT ( 'NONE', #11636 ) ;
#6979=DIRECTION ( 'NONE',  ( 1.169602638241521591E-15, -0.1872998510044552312, -0.9823027872370662106 ) ) ;
#6989=CYLINDRICAL_SURFACE ( 'NONE', #11968, 0.2000000000000012046 ) ;
#6991=EDGE_CURVE ( 'NONE', #10870, #8351, #4760, .T. ) ;
#7000=ORIENTED_EDGE ( 'NONE', *, *, #12080, .T. ) ;
#7034=CARTESIAN_POINT ( 'NONE',  ( -15.13173615696983276, -107.1622034095870077, -6.087689735156000204 ) ) ;
#7102=ORIENTED_EDGE ( 'NONE', *, *, #12455, .F. ) ;
#7117=ORIENTED_EDGE ( 'NONE', *, *, #12080, .F. ) ;
#7122=VECTOR ( 'NONE', #7398, 1000.000000000000000 ) ;
#7134=CARTESIAN_POINT ( 'NONE',  ( -14.76203582817000282, -106.8625236479798843, -4.516005275576693734 ) ) ;
#7146=ADVANCED_FACE ( 'NONE', ( #6192 ), #402, .T. ) ;
#7148=DIRECTION ( 'NONE',  ( -1.000000000000000000, -1.201369187114119994E-15, -9.616040805000176517E-16 ) ) ;
#7167=ADVANCED_FACE ( 'NONE', ( #4991 ), #8716, .T. ) ;
#7170=EDGE_CURVE ( 'NONE', #6540, #15034, #9650, .T. ) ;
#7181=DIRECTION ( 'NONE',  ( -1.000000000000000000, -1.201369187114119994E-15, -9.616040805000176517E-16 ) ) ;
#7183=ORIENTED_EDGE ( 'NONE', *, *, #10207, .T. ) ;
#7184=DIRECTION ( 'NONE',  ( -1.000000000000000000, -1.201369187114119994E-15, -9.616040805000176517E-16 ) ) ;
#7190=EDGE_CURVE ( 'NONE', #8640, #11007, #7436, .T. ) ;
#7227=VERTEX_POINT ( 'NONE', #8940 ) ;
#7236=DIRECTION ( 'NONE',  ( 0.000000000000000000, 0.1872998510044759646, 0.9823027872370621028 ) ) ;
#7252=DIRECTION ( 'NONE',  ( 0.000000000000000000, 0.1872998510044689147, 0.9823027872370635460 ) ) ;
#7272=DIRECTION ( 'NONE',  ( 1.000000000000000000, 1.201369187114119994E-15, 9.616040805000176517E-16 ) ) ;
#7300=VERTEX_POINT ( 'NONE', #4899 ) ;
#7327=ORIENTED_EDGE ( 'NONE', *, *, #14773, .T. ) ;
#7329=DIRECTION ( 'NONE',  ( 0.000000000000000000, 0.1872998510044759646, 0.9823027872370621028 ) ) ;
#7339=FACE_OUTER_BOUND ( 'NONE', #8599, .T. ) ;
#7361=AXIS2_PLACEMENT_3D ( 'NONE', #9758, #1717, #6369 ) ;
#7385=CYLINDRICAL_SURFACE ( 'NONE', #3007, 0.4500000000000011768 ) ;
#7398=DIRECTION ( 'NONE',  ( 1.000000000000000000, 1.201369187114119994E-15, 9.616040805000176517E-16 ) ) ;
#7401=AXIS2_PLACEMENT_3D ( 'NONE', #4833, #7181, #7252 ) ;
#7413=VERTEX_POINT ( 'NONE', #14576 ) ;
#7431=ADVANCED_FACE ( 'NONE', ( #2869 ), #3532, .T. ) ;
#7436=CIRCLE ( 'NONE', #6693, 0.2000000000000012046 ) ;
#7446=DIRECTION ( 'NONE',  ( 0.000000000000000000, 0.1872998510044689147, 0.9823027872370635460 ) ) ;
#7461=MANIFOLD_SOLID_BREP ( 'Stock-MAS-672-1', #8769 ) ;
#7490=CARTESIAN_POINT ( 'NONE',  ( -15.61203582816999713, -107.9994814593942607, -7.057848339359948042 ) ) ;
#7507=CARTESIAN_POINT ( 'NONE',  ( -15.61203582816999891, -108.0739289917895007, -5.561265332623595015 ) ) ;
#7524=VECTOR ( 'NONE', #14145, 1000.000000000000000 ) ;
#7565=CARTESIAN_POINT ( 'NONE',  ( -14.61203582817000068, -107.1622034095870077, -6.087689735155999315 ) ) ;
#7589=DIRECTION ( 'NONE',  ( -1.000000000000000000, -1.201369187114119994E-15, -9.616040805000176517E-16 ) ) ;
#7613=DIRECTION ( 'NONE',  ( 1.000000000000000000, 1.201369187114119994E-15, 9.616040805000176517E-16 ) ) ;
#7620=ADVANCED_FACE ( 'NONE', ( #8440 ), #1966, .T. ) ;
#7660=DIRECTION ( 'NONE',  ( 1.982541115402064518E-15, -0.1872998510044552312, -0.9823027872370662106 ) ) ;
#7694=LINE ( 'NONE', #11153, #421 ) ;
#7701=PLANE ( 'NONE',  #10953 ) ;
#7706=CARTESIAN_POINT ( 'NONE',  ( -15.61203582816999891, -108.2036686363109084, -6.241690937583108223 ) ) ;
#7710=VECTOR ( 'NONE', #5576, 1000.000000000000000 ) ;
#7712=ADVANCED_FACE ( 'NONE', ( #12114 ), #8663, .T. ) ;
#7737=VERTEX_POINT ( 'NONE', #1629 ) ;
#7739=VERTEX_POINT ( 'NONE', #6505 ) ;
#7746=ADVANCED_FACE ( 'NONE', ( #13273 ), #2782, .T. ) ;
#7750=CARTESIAN_POINT ( 'NONE',  ( -15.09158957740191553, -107.4899781488447843, -7.806719612820868903 ) ) ;
#7762=CYLINDRICAL_SURFACE ( 'NONE', #2172, 0.4500000000000011768 ) ;
#7764=CARTESIAN_POINT ( 'NONE',  ( -15.11203582817000068, -107.1622034095870077, -6.087689735156000204 ) ) ;
#7769=LINE ( 'NONE', #827, #4383 ) ;
#7782=VERTEX_POINT ( 'NONE', #13639 ) ;
#7794=ORIENTED_EDGE ( 'NONE', *, *, #5649, .T. ) ;
#7804=AXIS2_PLACEMENT_3D ( 'NONE', #2849, #7589, #7660 ) ;
#7823=CYLINDRICAL_SURFACE ( 'NONE', #13161, 0.4500000000000011768 ) ;
#7860=AXIS2_PLACEMENT_3D ( 'NONE', #4640, #11596, #1112 ) ;
#7867=VERTEX_POINT ( 'NONE', #5819 ) ;
#7904=CYLINDRICAL_SURFACE ( 'NONE', #13315, 0.2000000000000012046 ) ;
#7907=FACE_OUTER_BOUND ( 'NONE', #6554, .T. ) ;
#7922=DIRECTION ( 'NONE',  ( 0.000000000000000000, 0.1872998510044689147, 0.9823027872370635460 ) ) ;
#7946=VERTEX_POINT ( 'NONE', #6039 ) ;
#7959=EDGE_LOOP ( 'NONE', ( #488, #14806, #11131, #2857 ) ) ;
#7967=DIRECTION ( 'NONE',  ( 1.000000000000000000, 1.201369187114119994E-15, 9.616040805000176517E-16 ) ) ;
#8022=DIRECTION ( 'NONE',  ( 0.000000000000000000, 0.1872998510044759646, 0.9823027872370621028 ) ) ;
#8023=EDGE_LOOP ( 'NONE', ( #9885, #12829, #8432, #575 ) ) ;
#8049=FACE_OUTER_BOUND ( 'NONE', #8183, .T. ) ;
#8071=DIRECTION ( 'NONE',  ( 0.000000000000000000, -0.1872998510044521503, -0.9823027872370667657 ) ) ;
#8102=EDGE_CURVE ( 'NONE', #4677, #14676, #2913, .T. ) ;
#8107=AXIS2_PLACEMENT_3D ( 'NONE', #11517, #5700, #10369 ) ;
#8122=ORIENTED_EDGE ( 'NONE', *, *, #14522, .T. ) ;
#8126=EDGE_LOOP ( 'NONE', ( #4700, #14737, #8644, #14639 ) ) ;
#8143=FACE_OUTER_BOUND ( 'NONE', #776, .T. ) ;
#8183=EDGE_LOOP ( 'NONE', ( #5697, #2840, #9678, #13600 ) ) ;
#8186=DIRECTION ( 'NONE',  ( -1.000000000000000472E-15, 0.9823027872370664326, -0.1872998510044540932 ) ) ;
#8240=DIRECTION ( 'NONE',  ( 0.000000000000000000, 0.1872998510044689147, 0.9823027872370635460 ) ) ;
#8253=AXIS2_PLACEMENT_3D ( 'NONE', #13841, #9165, #1986 ) ;
#8268=DIRECTION ( 'NONE',  ( 9.943800201373337757E-16, -0.1872998510044509290, -0.9823027872370669877 ) ) ;
#8276=EDGE_CURVE ( 'NONE', #645, #1981, #5060, .T. ) ;
#8299=AXIS2_PLACEMENT_3D ( 'NONE', #9183, #9035, #14785 ) ;
#8328=CARTESIAN_POINT ( 'NONE',  ( -17.61203582817000068, -107.1622034095870077, -6.087689735156001980 ) ) ;
#8351=VERTEX_POINT ( 'NONE', #5800 ) ;
#8375=CIRCLE ( 'NONE', #7401, 0.4500000000000011768 ) ;
#8432=ORIENTED_EDGE ( 'NONE', *, *, #8276, .F. ) ;
#8433=EDGE_LOOP ( 'NONE', ( #2598, #10521, #4483, #2037 ) ) ;
#8440=FACE_OUTER_BOUND ( 'NONE', #2880, .T. ) ;
#8468=ORIENTED_EDGE ( 'NONE', *, *, #14204, .F. ) ;
#8471=AXIS2_PLACEMENT_3D ( 'NONE', #1326, #7272, #342 ) ;
#8482=CARTESIAN_POINT ( 'NONE',  ( -14.61203582817000068, -106.2504778273845147, -6.614114137688406281 ) ) ;
#8532=ADVANCED_FACE ( 'NONE', ( #12459 ), #4421, .T. ) ;
#8553=EDGE_CURVE ( 'NONE', #6540, #11437, #7694, .T. ) ;
#8569=PRODUCT_CONTEXT ( 'NONE', #4007, 'mechanical' ) ;
#8599=EDGE_LOOP ( 'NONE', ( #718, #11979 ) ) ;
#8611=EDGE_CURVE ( 'NONE', #10009, #7867, #9703, .T. ) ;
#8616=CIRCLE ( 'NONE', #11966, 1.744527686444488968 ) ;
#8625=EDGE_LOOP ( 'NONE', ( #14062, #13649, #13595, #9808 ) ) ;
#8640=VERTEX_POINT ( 'NONE', #10784 ) ;
#8644=ORIENTED_EDGE ( 'NONE', *, *, #6147, .T. ) ;
#8663=CYLINDRICAL_SURFACE ( 'NONE', #7804, 1.750000000000000666 ) ;
#8716=CYLINDRICAL_SURFACE ( 'NONE', #1338, 0.4500000000000011768 ) ;
#8739=DIRECTION ( 'NONE',  ( 1.000000000000000275E-15, -0.9823027872370663216, 0.1872998510044540654 ) ) ;
#8767=ORIENTED_EDGE ( 'NONE', *, *, #8102, .T. ) ;
#8769=CLOSED_SHELL ( 'NONE', ( #11863, #7431, #3172, #9036, #11684, #14118, #7167, #8532, #6020, #7620, #9087, #11398, #10278, #2521, #1593, #4213, #2591, #3249, #2210, #1027, #1963, #4023, #13461, #10356, #327, #14425, #7746, #7712, #10176, #7146, #3626, #571 ) ) ;
#8775=CARTESIAN_POINT ( 'NONE',  ( -15.61203582816999891, -107.3496051183401647, -7.070526720097524809 ) ) ;
#8791=DIRECTION ( 'NONE',  ( 1.000000000000000000, 1.201369187114119994E-15, 9.616040805000176517E-16 ) ) ;
#8819=EDGE_LOOP ( 'NONE', ( #12955, #2358, #4564, #7102 ) ) ;
#8832=DIRECTION ( 'NONE',  ( 1.000000000000000000, 1.201369187114119994E-15, 9.616040805000176517E-16 ) ) ;
#8841=CIRCLE ( 'NONE', #13013, 0.4500000000000011768 ) ;
#8843=VECTOR ( 'NONE', #766, 1000.000000000000000 ) ;
#8848=DIRECTION ( 'NONE',  ( -1.000000000000000000, -1.201369187114119994E-15, -9.616040805000176517E-16 ) ) ;
#8850=VECTOR ( 'NONE', #6117, 1000.000000000000000 ) ;
#8853=ORIENTED_EDGE ( 'NONE', *, *, #11055, .F. ) ;
#8856=CARTESIAN_POINT ( 'NONE',  ( -20.61203582816999713, -107.3495032605914616, -7.069992522393071965 ) ) ;
#8891=( NAMED_UNIT ( * ) PLANE_ANGLE_UNIT ( ) SI_UNIT ( $, .RADIAN. ) );
#8912=DIRECTION ( 'NONE',  ( 1.000000000000000000, 1.201369187114119994E-15, 9.616040805000176517E-16 ) ) ;
#8940=CARTESIAN_POINT ( 'NONE',  ( -14.76203582817000104, -106.8344286703292170, -4.368659857491133280 ) ) ;
#8946=VERTEX_POINT ( 'NONE', #13150 ) ;
#8974=AXIS2_PLACEMENT_3D ( 'NONE', #1198, #6003, #139 ) ;
#8992=DIRECTION ( 'NONE',  ( 1.000000000000000000, 1.201369187114119994E-15, 9.616040805000176517E-16 ) ) ;
#9001=DIRECTION ( 'NONE',  ( 1.000000000000000000, 1.201369187114119994E-15, 9.616040805000176517E-16 ) ) ;
#9003=ORIENTED_EDGE ( 'NONE', *, *, #5579, .F. ) ;
#9032=ORIENTED_EDGE ( 'NONE', *, *, #2694, .F. ) ;
#9035=DIRECTION ( 'NONE',  ( 1.000000000000000000, 1.201369187114119994E-15, 9.616040805000176517E-16 ) ) ;
#9036=ADVANCED_FACE ( 'NONE', ( #144 ), #4804, .F. ) ;
#9070=CARTESIAN_POINT ( 'NONE',  ( -15.61203582816999891, -107.9196643519486969, -5.433976602192394090 ) ) ;
#9073=EDGE_CURVE ( 'NONE', #645, #1536, #13303, .T. ) ;
#9075=CARTESIAN_POINT ( 'NONE',  ( -16.91203582817000139, -107.1622034095870077, -6.087689735156001980 ) ) ;
#9077=AXIS2_PLACEMENT_3D ( 'NONE', #10427, #7967, #9195 ) ;
#9087=ADVANCED_FACE ( 'NONE', ( #5106 ), #5796, .T. ) ;
#9102=CARTESIAN_POINT ( 'NONE',  ( -15.61203582816999891, -106.7406604375499626, -7.297873098422156701 ) ) ;
#9110=VERTEX_POINT ( 'NONE', #3952 ) ;
#9126=DIRECTION ( 'NONE',  ( 0.000000000000000000, 0.1872998510044759646, 0.9823027872370621028 ) ) ;
#9146=AXIS2_PLACEMENT_3D ( 'NONE', #9724, #6415, #1685 ) ;
#9165=DIRECTION ( 'NONE',  ( 1.000000000000000000, 1.201369187114119994E-15, 9.616040805000176517E-16 ) ) ;
#9172=EDGE_LOOP ( 'NONE', ( #12412, #5643, #12468, #2683 ) ) ;
#9183=CARTESIAN_POINT ( 'NONE',  ( -15.61203582817000068, -105.9033823877427096, -6.327714494218207975 ) ) ;
#9192=EDGE_LOOP ( 'NONE', ( #611, #7327, #12467, #12713 ) ) ;
#9195=DIRECTION ( 'NONE',  ( 0.000000000000000000, 0.1872998510044759646, 0.9823027872370621028 ) ) ;
#9197=DIRECTION ( 'NONE',  ( 1.000000000000000000, 1.201369187114119994E-15, 9.616040805000176517E-16 ) ) ;
#9199=SURFACE_STYLE_FILL_AREA ( #15024 ) ;
#9212=DIRECTION ( 'NONE',  ( 1.000000000000000000, 1.201369187114119994E-15, 9.616040805000176517E-16 ) ) ;
#9222=EDGE_CURVE ( 'NONE', #15001, #5098, #4841, .T. ) ;
#9227=CARTESIAN_POINT ( 'NONE',  ( -15.61203582817000068, -106.2504778273845147, -6.614114137688407169 ) ) ;
#9253=VECTOR ( 'NONE', #5365, 1000.000000000000000 ) ;
#9254=ORIENTED_EDGE ( 'NONE', *, *, #2818, .F. ) ;
#9293=FACE_OUTER_BOUND ( 'NONE', #8819, .T. ) ;
#9301=DIRECTION ( 'NONE',  ( 1.000000000000000000, 1.201369187114119994E-15, 9.616040805000176517E-16 ) ) ;
#9340=CARTESIAN_POINT ( 'NONE',  ( -15.09158957740191909, -106.8625236479798843, -4.516005275576694622 ) ) ;
#9366=CARTESIAN_POINT ( 'NONE',  ( -16.91203582817000139, -107.1622034095870077, -6.087689735156001980 ) ) ;
#9397=ORIENTED_EDGE ( 'NONE', *, *, #1121, .T. ) ;
#9418=DIRECTION ( 'NONE',  ( 1.000000000000000000, 1.201369187114119994E-15, 9.616040805000176517E-16 ) ) ;
#9428=ORIENTED_EDGE ( 'NONE', *, *, #14355, .F. ) ;
#9431=VERTEX_POINT ( 'NONE', #9445 ) ;
#9438=AXIS2_PLACEMENT_3D ( 'NONE', #1072, #2299, #4822 ) ;
#9445=CARTESIAN_POINT ( 'NONE',  ( -14.61203582817000246, -106.2504437127206529, -5.561324420954689707 ) ) ;
#9469=CARTESIAN_POINT ( 'NONE',  ( -15.61203582816999891, -106.6563755045979605, -6.855836844165477117 ) ) ;
#9501=LINE ( 'NONE', #1471, #8850 ) ;
#9512=VECTOR ( 'NONE', #2652, 1000.000000000000000 ) ;
#9514=CARTESIAN_POINT ( 'NONE',  ( -14.76203582817000104, -107.1622034095870077, -6.087689735155999315 ) ) ;
#9557=AXIS2_PLACEMENT_3D ( 'NONE', #5015, #12977, #5990 ) ;
#9563=DIRECTION ( 'NONE',  ( -1.000000000000000000, -1.201369187114119994E-15, -9.616040805000176517E-16 ) ) ;
#9565=ORIENTED_EDGE ( 'NONE', *, *, #10656, .T. ) ;
#9596=FACE_BOUND ( 'NONE', #148, .T. ) ;
#9597=EDGE_LOOP ( 'NONE', ( #11026, #3480, #3754, #3846 ) ) ;
#9606=AXIS2_PLACEMENT_3D ( 'NONE', #3371, #6941, #8022 ) ;
#9622=DIRECTION ( 'NONE',  ( -1.000000000000000000, -1.201369187114119994E-15, -9.616040805000176517E-16 ) ) ;
#9636=EDGE_CURVE ( 'NONE', #5900, #11437, #6736, .T. ) ;
#9650=LINE ( 'NONE', #2982, #10877 ) ;
#9655=CARTESIAN_POINT ( 'NONE',  ( -20.61203582816999713, -107.1622034095870077, -6.087689735156005533 ) ) ;
#9663=ORIENTED_EDGE ( 'NONE', *, *, #14355, .T. ) ;
#9678=ORIENTED_EDGE ( 'NONE', *, *, #4536, .F. ) ;
#9703=CIRCLE ( 'NONE', #3837, 0.2000000000000012046 ) ;
#9715=AXIS2_PLACEMENT_3D ( 'NONE', #14735, #4032, #736 ) ;
#9724=CARTESIAN_POINT ( 'NONE',  ( -17.61203582817000068, -107.1622034095870077, -6.087689735156001980 ) ) ;
#9737=ORIENTED_EDGE ( 'NONE', *, *, #14574, .T. ) ;
#9742=VECTOR ( 'NONE', #10666, 1000.000000000000000 ) ;
#9749=PLANE ( 'NONE',  #12570 ) ;
#9758=CARTESIAN_POINT ( 'NONE',  ( -14.76203582816999926, -107.4618831711941169, -7.659374194735305785 ) ) ;
#9780=FACE_OUTER_BOUND ( 'NONE', #7959, .T. ) ;
#9808=ORIENTED_EDGE ( 'NONE', *, *, #9636, .F. ) ;
#9824=ORIENTED_EDGE ( 'NONE', *, *, #7170, .T. ) ;
#9828=EDGE_LOOP ( 'NONE', ( #4391, #14161, #10027, #14441 ) ) ;
#9876=DIRECTION ( 'NONE',  ( -1.000000000000000000, -1.201369187114119994E-15, -9.616040805000176517E-16 ) ) ;
#9885=ORIENTED_EDGE ( 'NONE', *, *, #2920, .T. ) ;
#9915=EDGE_LOOP ( 'NONE', ( #3980, #11996, #3696, #3901 ) ) ;
#9938=TOROIDAL_SURFACE ( 'NONE', #8471, 1.600000000000000089, 0.1499999999999999944 ) ;
#9964=VERTEX_POINT ( 'NONE', #6718 ) ;
#9999=LINE ( 'NONE', #13606, #13104 ) ;
#10009=VERTEX_POINT ( 'NONE', #6870 ) ;
#10027=ORIENTED_EDGE ( 'NONE', *, *, #6198, .T. ) ;
#10076=DIRECTION ( 'NONE',  ( 1.000000000000000000, 1.201369187114119994E-15, 9.616040805000176517E-16 ) ) ;
#10083=EDGE_CURVE ( 'NONE', #5848, #6974, #2304, .T. ) ;
#10088=EDGE_CURVE ( 'NONE', #7300, #9964, #5651, .T. ) ;
#10104=AXIS2_PLACEMENT_3D ( 'NONE', #3071, #12411, #1929 ) ;
#10122=SURFACE_SIDE_STYLE ('',( #9199 ) ) ;
#10144=DIRECTION ( 'NONE',  ( 0.000000000000000000, 0.1872998510044759646, 0.9823027872370621028 ) ) ;
#10168=AXIS2_PLACEMENT_3D ( 'NONE', #11453, #6618, #7922 ) ;
#10170=SHAPE_REPRESENTATION ( 'Insert Torx Screw', ( #6789 ), #4860 ) ;
#10176=ADVANCED_FACE ( 'NONE', ( #13246 ), #5181, .T. ) ;
#10207=EDGE_CURVE ( 'NONE', #6401, #13230, #8841, .T. ) ;
#10256=VERTEX_POINT ( 'NONE', #5548 ) ;
#10258=APPLICATION_CONTEXT ( 'automotive_design' ) ;
#10260=DIRECTION ( 'NONE',  ( 1.000000000000000000, 1.201369187114119994E-15, 9.616040805000176517E-16 ) ) ;
#10278=ADVANCED_FACE ( 'NONE', ( #9293 ), #14951, .T. ) ;
#10332=ORIENTED_EDGE ( 'NONE', *, *, #6340, .F. ) ;
#10337=EDGE_CURVE ( 'NONE', #4677, #7227, #12525, .T. ) ;
#10356=ADVANCED_FACE ( 'NONE', ( #8143 ), #6911, .F. ) ;
#10361=DIRECTION ( 'NONE',  ( 0.000000000000000000, 0.1872998510044759646, 0.9823027872370621028 ) ) ;
#10369=DIRECTION ( 'NONE',  ( 9.912705577010322591E-16, -0.1872998510044552312, -0.9823027872370662106 ) ) ;
#10376=( GEOMETRIC_REPRESENTATION_CONTEXT ( 3 ) GLOBAL_UNCERTAINTY_ASSIGNED_CONTEXT ( ( #370 ) ) GLOBAL_UNIT_ASSIGNED_CONTEXT ( ( #958, #13884, #5535 ) ) REPRESENTATION_CONTEXT ( 'NONE', 'WORKASPACE' ) );
#10378=DIRECTION ( 'NONE',  ( 0.000000000000000000, 0.1872998510044689147, 0.9823027872370635460 ) ) ;
#10421=CARTESIAN_POINT ( 'NONE',  ( -20.61203582816999713, -106.9749035585825681, -5.105386947918939100 ) ) ;
#10427=CARTESIAN_POINT ( 'NONE',  ( -14.61203582817000246, -106.9748017008338365, -5.104852750214475599 ) ) ;
#10439=DIRECTION ( 'NONE',  ( 0.000000000000000000, 0.1872998510044759646, 0.9823027872370621028 ) ) ;
#10456=DIRECTION ( 'NONE',  ( 1.000000000000000000, 1.201369187114119994E-15, 9.616040805000176517E-16 ) ) ;
#10482=CYLINDRICAL_SURFACE ( 'NONE', #5447, 1.249999999999999778 ) ;
#10497=VECTOR ( 'NONE', #14053, 1000.000000000000000 ) ;
#10500=ORIENTED_EDGE ( 'NONE', *, *, #73, .F. ) ;
#10521=ORIENTED_EDGE ( 'NONE', *, *, #1583, .T. ) ;
#10528=CARTESIAN_POINT ( 'NONE',  ( -20.36203582816999713, -107.1622034095870077, -6.087689735156004645 ) ) ;
#10543=EDGE_CURVE ( 'NONE', #12074, #10009, #4452, .T. ) ;
#10555=CARTESIAN_POINT ( 'NONE',  ( -15.61203582817000068, -107.8163049764641812, -5.262754992868533321 ) ) ;
#10580=EDGE_LOOP ( 'NONE', ( #11201, #12128, #9824, #12238 ) ) ;
#10620=EDGE_LOOP ( 'NONE', ( #146, #6102 ) ) ;
#10634=ORIENTED_EDGE ( 'NONE', *, *, #5649, .F. ) ;
#10636=ORIENTED_EDGE ( 'NONE', *, *, #14341, .T. ) ;
#10656=EDGE_CURVE ( 'NONE', #10870, #5903, #11789, .T. ) ;
#10666=DIRECTION ( 'NONE',  ( 1.000000000000000000, 1.201369187114119994E-15, 9.616040805000176517E-16 ) ) ;
#10699=AXIS2_PLACEMENT_3D ( 'NONE', #5743, #7184, #11786 ) ;
#10706=DIRECTION ( 'NONE',  ( 1.000000000000000000, 1.201369187114119994E-15, 9.616040805000176517E-16 ) ) ;
#10709=DIRECTION ( 'NONE',  ( -1.000000000000000000, -1.201369187114119994E-15, -9.616040805000176517E-16 ) ) ;
#10739=CIRCLE ( 'NONE', #5843, 0.2000000000000012046 ) ;
#10746=CARTESIAN_POINT ( 'NONE',  ( -15.61203582817000068, -106.7748397497402806, -5.108753790441425302 ) ) ;
#10762=CARTESIAN_POINT ( 'NONE',  ( -15.61203582816999891, -107.9196643519486969, -5.433976602192394090 ) ) ;
#10777=VERTEX_POINT ( 'NONE', #2628 ) ;
#10780=EDGE_CURVE ( 'NONE', #633, #1609, #14202, .T. ) ;
#10784=CARTESIAN_POINT ( 'NONE',  ( -14.61203582816999891, -108.2036686363109084, -6.241690937583107335 ) ) ;
#10813=CARTESIAN_POINT ( 'NONE',  ( -15.61203582816999713, -107.9994814593942607, -7.057848339359948042 ) ) ;
#10831=ORIENTED_EDGE ( 'NONE', *, *, #14592, .T. ) ;
#10854=DIRECTION ( 'NONE',  ( 0.000000000000000000, 0.1872998510044759646, 0.9823027872370621028 ) ) ;
#10862=ORIENTED_EDGE ( 'NONE', *, *, #4775, .T. ) ;
#10870=VERTEX_POINT ( 'NONE', #3417 ) ;
#10877=VECTOR ( 'NONE', #5134, 999.9999999999998863 ) ;
#10882=CARTESIAN_POINT ( 'NONE',  ( -20.36203582816999713, -106.9280785958314510, -4.859811251109673158 ) ) ;
#10913=ORIENTED_EDGE ( 'NONE', *, *, #6341, .F. ) ;
#10948=DIRECTION ( 'NONE',  ( 0.000000000000000000, 0.1872998510044759646, 0.9823027872370621028 ) ) ;
#10953=AXIS2_PLACEMENT_3D ( 'NONE', #5414, #10076, #3123 ) ;
#10981=CYLINDRICAL_SURFACE ( 'NONE', #6396, 0.2000000000000012046 ) ;
#10987=DIRECTION ( 'NONE',  ( -1.000000000000000000, -1.201369187114119994E-15, -9.616040805000176517E-16 ) ) ;
#10995=ORIENTED_EDGE ( 'NONE', *, *, #5943, .F. ) ;
#11007=VERTEX_POINT ( 'NONE', #14713 ) ;
#11026=ORIENTED_EDGE ( 'NONE', *, *, #14674, .T. ) ;
#11027=VERTEX_POINT ( 'NONE', #2710 ) ;
#11040=PRODUCT_DEFINITION_SHAPE ( 'NONE', 'NONE',  #11525 ) ;
#11055=EDGE_CURVE ( 'NONE', #1609, #7946, #5644, .T. ) ;
#11058=VECTOR ( 'NONE', #6955, 1000.000000000000000 ) ;
#11084=LINE ( 'NONE', #4123, #923 ) ;
#11102=EDGE_CURVE ( 'NONE', #11853, #9110, #4685, .T. ) ;
#11131=ORIENTED_EDGE ( 'NONE', *, *, #6341, .T. ) ;
#11134=CARTESIAN_POINT ( 'NONE',  ( -15.11203582817000068, -107.1622034095870077, -6.087689735156000204 ) ) ;
#11135=CARTESIAN_POINT ( 'NONE',  ( -14.61203582817000068, -107.5837463816240529, -4.877506371889843706 ) ) ;
#11153=CARTESIAN_POINT ( 'NONE',  ( -17.61203582817000068, -106.9280785958314368, -4.859811251109668717 ) ) ;
#11197=DIRECTION ( 'NONE',  ( 1.000000000000000000, 1.201369187114119994E-15, 9.616040805000176517E-16 ) ) ;
#11201=ORIENTED_EDGE ( 'NONE', *, *, #1583, .F. ) ;
#11218=CARTESIAN_POINT ( 'NONE',  ( -15.61203582816999891, -107.5495670694337207, -7.066625679870576882 ) ) ;
#11219=CIRCLE ( 'NONE', #11454, 0.4500000000000011768 ) ;
#11228=EDGE_CURVE ( 'NONE', #13230, #1495, #4309, .T. ) ;
#11242=ORIENTED_EDGE ( 'NONE', *, *, #8553, .F. ) ;
#11280=DIRECTION ( 'NONE',  ( 0.000000000000000000, 0.1872998510044689147, 0.9823027872370635460 ) ) ;
#11298=AXIS2_PLACEMENT_3D ( 'NONE', #5180, #300, #10854 ) ;
#11320=AXIS2_PLACEMENT_3D ( 'NONE', #2337, #11588, #1105 ) ;
#11326=AXIS2_PLACEMENT_3D ( 'NONE', #3662, #9622, #6013 ) ;
#11328=EDGE_LOOP ( 'NONE', ( #2773, #5608, #2717, #9428 ) ) ;
#11331=DIRECTION ( 'NONE',  ( 0.000000000000000000, 0.1872998510044689147, 0.9823027872370635460 ) ) ;
#11394=EDGE_CURVE ( 'NONE', #7739, #1092, #9501, .T. ) ;
#11398=ADVANCED_FACE ( 'NONE', ( #2693 ), #12048, .T. ) ;
#11437=VERTEX_POINT ( 'NONE', #10882 ) ;
#11453=CARTESIAN_POINT ( 'NONE',  ( -15.61203582816999891, -106.7406604375499626, -7.297873098422156701 ) ) ;
#11454=AXIS2_PLACEMENT_3D ( 'NONE', #6120, #13339, #5140 ) ;
#11472=DIRECTION ( 'NONE',  ( 1.000000000000000000, 1.201369187114119994E-15, 9.616040805000176517E-16 ) ) ;
#11473=CARTESIAN_POINT ( 'NONE',  ( -14.61203582817000068, -106.6563755045979605, -6.855836844165474453 ) ) ;
#11488=CARTESIAN_POINT ( 'NONE',  ( -15.61203582817000068, -106.4047424672253186, -6.741402868119606318 ) ) ;
#11517=CARTESIAN_POINT ( 'NONE',  ( -14.76203582817000104, -107.1622034095870077, -6.087689735155999315 ) ) ;
#11524=CARTESIAN_POINT ( 'NONE',  ( -14.61203582817000068, -106.7406604375499626, -7.297873098422155813 ) ) ;
#11525=PRODUCT_DEFINITION ( 'UNKNOWN', '', #3893, #4830 ) ;
#11527=DIRECTION ( 'NONE',  ( 0.000000000000000000, 0.1872998510044689147, 0.9823027872370635460 ) ) ;
#11588=DIRECTION ( 'NONE',  ( -1.000000000000000000, -1.201369187114119994E-15, -9.616040805000176517E-16 ) ) ;
#11596=DIRECTION ( 'NONE',  ( 1.000000000000000000, 1.201369187114119994E-15, 9.616040805000176517E-16 ) ) ;
#11610=CARTESIAN_POINT ( 'NONE',  ( -15.61203582816999713, -108.0739631064533484, -6.614055049357310700 ) ) ;
#11636=CARTESIAN_POINT ( 'NONE',  ( -14.61203582817000068, -107.8163049764641812, -5.262754992868532433 ) ) ;
#11654=PRESENTATION_STYLE_ASSIGNMENT (( #5687 ) ) ;
#11670=DIRECTION ( 'NONE',  ( 0.000000000000000000, 0.1872998510044689147, 0.9823027872370635460 ) ) ;
#11684=ADVANCED_FACE ( 'NONE', ( #13850 ), #6643, .F. ) ;
#11716=CIRCLE ( 'NONE', #245, 0.4500000000000011768 ) ;
#11747=AXIS2_PLACEMENT_3D ( 'NONE', #3848, #6126, #13898 ) ;
#11755=ORIENTED_EDGE ( 'NONE', *, *, #14674, .F. ) ;
#11760=VECTOR ( 'NONE', #14078, 1000.000000000000000 ) ;
#11764=DIRECTION ( 'NONE',  ( 1.000000000000000000, 1.201369187114119994E-15, 9.616040805000176517E-16 ) ) ;
#11770=AXIS2_PLACEMENT_3D ( 'NONE', #7764, #466, #5124 ) ;
#11786=DIRECTION ( 'NONE',  ( 0.000000000000000000, 0.1872998510044689147, 0.9823027872370635460 ) ) ;
#11789=CIRCLE ( 'NONE', #556, 0.2000000000000012046 ) ;
#11797=AXIS2_PLACEMENT_3D ( 'NONE', #9655, #14095, #13038 ) ;
#11819=EDGE_LOOP ( 'NONE', ( #11242, #6664, #10831, #9663 ) ) ;
#11829=LINE ( 'NONE', #11905, #9512 ) ;
#11830=CIRCLE ( 'NONE', #5467, 0.4500000000000011768 ) ;
#11853=VERTEX_POINT ( 'NONE', #3676 ) ;
#11863=ADVANCED_FACE ( 'NONE', ( #5806 ), #10482, .T. ) ;
#11870=EDGE_CURVE ( 'NONE', #8946, #3470, #2899, .T. ) ;
#11905=CARTESIAN_POINT ( 'NONE',  ( -17.61203582817000068, -107.3963282233425645, -7.315568219202336131 ) ) ;
#11961=ORIENTED_EDGE ( 'NONE', *, *, #10207, .F. ) ;
#11966=AXIS2_PLACEMENT_3D ( 'NONE', #1628, #14557, #5079 ) ;
#11968=AXIS2_PLACEMENT_3D ( 'NONE', #6845, #9301, #5779 ) ;
#11979=ORIENTED_EDGE ( 'NONE', *, *, #866, .T. ) ;
#11990=CARTESIAN_POINT ( 'NONE',  ( -20.36203582816999713, -107.3963282233425787, -7.315568219202339684 ) ) ;
#11996=ORIENTED_EDGE ( 'NONE', *, *, #14204, .T. ) ;
#12020=CARTESIAN_POINT ( 'NONE',  ( -20.61203582816999713, -107.2792658164648003, -6.701628977179171720 ) ) ;
#12021=ORIENTED_EDGE ( 'NONE', *, *, #10337, .T. ) ;
#12041=ORIENTED_EDGE ( 'NONE', *, *, #1971, .T. ) ;
#12048=CONICAL_SURFACE ( 'NONE', #11797, 0.9999999999999990008, 0.7853981633974476129 ) ;
#12049=DIRECTION ( 'NONE',  ( 0.000000000000000000, -0.1872998510044090459, -0.9823027872370749813 ) ) ;
#12065=DIRECTION ( 'NONE',  ( 1.000000000000000000, 1.201369187114119994E-15, 9.616040805000176517E-16 ) ) ;
#12070=DIRECTION ( 'NONE',  ( 0.000000000000000000, 0.1872998510044689147, 0.9823027872370635460 ) ) ;
#12074=VERTEX_POINT ( 'NONE', #14239 ) ;
#12079=EDGE_CURVE ( 'NONE', #1553, #8640, #8375, .T. ) ;
#12080=EDGE_CURVE ( 'NONE', #12967, #1536, #1309, .T. ) ;
#12081=CIRCLE ( 'NONE', #4747, 1.744527686444488968 ) ;
#12098=DIRECTION ( 'NONE',  ( 1.000000000000000000, 1.201369187114119994E-15, 9.616040805000176517E-16 ) ) ;
#12099=DIRECTION ( 'NONE',  ( 1.000000000000000000, 1.201369187114119994E-15, 9.616040805000176517E-16 ) ) ;
#12107=ORIENTED_EDGE ( 'NONE', *, *, #6289, .F. ) ;
#12114=FACE_OUTER_BOUND ( 'NONE', #394, .T. ) ;
#12123=ORIENTED_EDGE ( 'NONE', *, *, #5579, .T. ) ;
#12127=DIRECTION ( 'NONE',  ( 0.000000000000000000, 0.1872998510044689147, 0.9823027872370635460 ) ) ;
#12128=ORIENTED_EDGE ( 'NONE', *, *, #3365, .F. ) ;
#12167=DIRECTION ( 'NONE',  ( -1.169602638241520408E-15, 0.1872998510044540654, 0.9823027872370663216 ) ) ;
#12206=CARTESIAN_POINT ( 'NONE',  ( -15.61203582816999891, -107.9196643519486969, -5.433976602192394090 ) ) ;
#12238=ORIENTED_EDGE ( 'NONE', *, *, #12962, .T. ) ;
#12260=ORIENTED_EDGE ( 'NONE', *, *, #2818, .T. ) ;
#12261=CARTESIAN_POINT ( 'NONE',  ( -20.61203582816999713, -106.9749035585825681, -5.105386947918939988 ) ) ;
#12283=ORIENTED_EDGE ( 'NONE', *, *, #3536, .T. ) ;
#12293=CARTESIAN_POINT ( 'NONE',  ( -15.09158957740191731, -107.1622034095870077, -6.087689735156000204 ) ) ;
#12320=CARTESIAN_POINT ( 'NONE',  ( -15.61203582816999891, -108.0739289917895007, -5.561265332623595015 ) ) ;
#12340=MECHANICAL_DESIGN_GEOMETRIC_PRESENTATION_REPRESENTATION('',(#15019),#10376);
#12343=CARTESIAN_POINT ( 'NONE',  ( -15.61203582817000068, -106.1798807882712765, -5.562105325730672511 ) ) ;
#12350=ORIENTED_EDGE ( 'NONE', *, *, #1447, .T. ) ;
#12365=CARTESIAN_POINT ( 'NONE',  ( -15.61203582817000068, -106.2173407584721616, -5.758565883178085265 ) ) ;
#12377=EDGE_CURVE ( 'NONE', #9431, #14723, #1321, .T. ) ;
#12380=DIRECTION ( 'NONE',  ( 1.000000000000000000, 1.201369187114119994E-15, 9.616040805000176517E-16 ) ) ;
#12402=CIRCLE ( 'NONE', #2876, 0.4500000000000011768 ) ;
#12411=DIRECTION ( 'NONE',  ( 1.000000000000000000, 1.201369187114119994E-15, 9.616040805000176517E-16 ) ) ;
#12412=ORIENTED_EDGE ( 'NONE', *, *, #4384, .F. ) ;
#12419=DIRECTION ( 'NONE',  ( 0.000000000000000000, 0.000000000000000000, 1.000000000000000000 ) ) ;
#12431=DIRECTION ( 'NONE',  ( 1.000000000000000000, 1.201369187114119994E-15, 9.616040805000176517E-16 ) ) ;
#12453=CIRCLE ( 'NONE', #13405, 1.599999999999999201 ) ;
#12455=EDGE_CURVE ( 'NONE', #7227, #4677, #5225, .T. ) ;
#12459=FACE_OUTER_BOUND ( 'NONE', #8126, .T. ) ;
#12467=ORIENTED_EDGE ( 'NONE', *, *, #1503, .T. ) ;
#12468=ORIENTED_EDGE ( 'NONE', *, *, #102, .F. ) ;
#12470=LINE ( 'NONE', #7706, #5186 ) ;
#12512=ORIENTED_EDGE ( 'NONE', *, *, #12962, .F. ) ;
#12517=CARTESIAN_POINT ( 'NONE',  ( -14.76203582817000104, -107.1622034095870077, -6.087689735155999315 ) ) ;
#12525=CIRCLE ( 'NONE', #8107, 1.750000000000000666 ) ;
#12543=ORIENTED_EDGE ( 'NONE', *, *, #2920, .F. ) ;
#12570=AXIS2_PLACEMENT_3D ( 'NONE', #3857, #13207, #8739 ) ;
#12577=CIRCLE ( 'NONE', #4022, 0.1500000000000015488 ) ;
#12594=DIRECTION ( 'NONE',  ( 1.000000000000000000, 1.201369187114119994E-15, 9.616040805000176517E-16 ) ) ;
#12650=EDGE_CURVE ( 'NONE', #6401, #15001, #3510, .T. ) ;
#12656=VERTEX_POINT ( 'NONE', #6761 ) ;
#12670=CIRCLE ( 'NONE', #8253, 1.750000000000000666 ) ;
#12671=ORIENTED_EDGE ( 'NONE', *, *, #5943, .T. ) ;
#12713=ORIENTED_EDGE ( 'NONE', *, *, #1488, .F. ) ;
#12758=CIRCLE ( 'NONE', #14363, 0.4500000000000011768 ) ;
#12761=FACE_OUTER_BOUND ( 'NONE', #9828, .T. ) ;
#12767=DIRECTION ( 'NONE',  ( -1.000000000000000000, -1.201369187114119994E-15, -9.616040805000176517E-16 ) ) ;
#12809=EDGE_CURVE ( 'NONE', #7737, #7739, #11830, .T. ) ;
#12829=ORIENTED_EDGE ( 'NONE', *, *, #14341, .F. ) ;
#12902=CIRCLE ( 'NONE', #4594, 0.2000000000000012046 ) ;
#12910=EDGE_LOOP ( 'NONE', ( #5683, #12512, #760, #13302 ) ) ;
#12915=EDGE_CURVE ( 'NONE', #11027, #7413, #3519, .T. ) ;
#12955=ORIENTED_EDGE ( 'NONE', *, *, #1121, .F. ) ;
#12962=EDGE_CURVE ( 'NONE', #15034, #12656, #12081, .T. ) ;
#12967=VERTEX_POINT ( 'NONE', #526 ) ;
#12977=DIRECTION ( 'NONE',  ( -1.000000000000000000, -1.201369187114119994E-15, -9.616040805000176517E-16 ) ) ;
#13013=AXIS2_PLACEMENT_3D ( 'NONE', #2345, #9212, #14891 ) ;
#13038=DIRECTION ( 'NONE',  ( 0.000000000000000000, 0.1872998510044495413, 0.9823027872370673208 ) ) ;
#13104=VECTOR ( 'NONE', #12380, 1000.000000000000000 ) ;
#13116=FACE_OUTER_BOUND ( 'NONE', #12910, .T. ) ;
#13125=DIRECTION ( 'NONE',  ( 1.169602638241521591E-15, -0.1872998510044552312, -0.9823027872370662106 ) ) ;
#13140=ORIENTED_EDGE ( 'NONE', *, *, #12079, .F. ) ;
#13150=CARTESIAN_POINT ( 'NONE',  ( -20.61203582816999713, -107.3495032605914616, -7.069992522393072854 ) ) ;
#13161=AXIS2_PLACEMENT_3D ( 'NONE', #14957, #13591, #14805 ) ;
#13163=CYLINDRICAL_SURFACE ( 'NONE', #13987, 0.2000000000000012046 ) ;
#13202=CIRCLE ( 'NONE', #1949, 0.4500000000000011768 ) ;
#13207=DIRECTION ( 'NONE',  ( -1.000000000000000000, -1.201369187114119994E-15, -9.616040805000176517E-16 ) ) ;
#13229=CARTESIAN_POINT ( 'NONE',  ( -14.61203582816999891, -107.9994814593942607, -7.057848339359947154 ) ) ;
#13230=VERTEX_POINT ( 'NONE', #9227 ) ;
#13232=ORIENTED_EDGE ( 'NONE', *, *, #3831, .T. ) ;
#13235=LINE ( 'NONE', #2743, #7122 ) ;
#13244=AXIS2_PLACEMENT_3D ( 'NONE', #13279, #11197, #3159 ) ;
#13246=FACE_OUTER_BOUND ( 'NONE', #10580, .T. ) ;
#13258=SHAPE_DEFINITION_REPRESENTATION ( #11040, #10170 ) ;
#13273=FACE_OUTER_BOUND ( 'NONE', #2283, .T. ) ;
#13279=CARTESIAN_POINT ( 'NONE',  ( -14.61203582817000246, -106.9748017008338365, -5.104852750214475599 ) ) ;
#13284=FACE_OUTER_BOUND ( 'NONE', #3565, .T. ) ;
#13287=DIRECTION ( 'NONE',  ( -1.000000000000000000, -1.201369187114119994E-15, -9.616040805000176517E-16 ) ) ;
#13302=ORIENTED_EDGE ( 'NONE', *, *, #1971, .F. ) ;
#13303=LINE ( 'NONE', #11218, #1896 ) ;
#13315=AXIS2_PLACEMENT_3D ( 'NONE', #3257, #12594, #10361 ) ;
#13339=DIRECTION ( 'NONE',  ( -1.000000000000000000, -1.201369187114119994E-15, -9.616040805000176517E-16 ) ) ;
#13347=AXIS2_PLACEMENT_3D ( 'NONE', #13459, #6549, #753 ) ;
#13361=CARTESIAN_POINT ( 'NONE',  ( -14.61203582817000246, -106.7748397497402806, -5.108753790441424414 ) ) ;
#13367=AXIS2_PLACEMENT_3D ( 'NONE', #6790, #11472, #996 ) ;
#13368=DIRECTION ( 'NONE',  ( 0.000000000000000000, 0.1872998510044689147, 0.9823027872370635460 ) ) ;
#13385=CYLINDRICAL_SURFACE ( 'NONE', #13347, 1.750000000000000666 ) ;
#13405=AXIS2_PLACEMENT_3D ( 'NONE', #7565, #12098, #3829 ) ;
#13412=ORIENTED_EDGE ( 'NONE', *, *, #14522, .F. ) ;
#13438=FACE_OUTER_BOUND ( 'NONE', #952, .T. ) ;
#13448=CARTESIAN_POINT ( 'NONE',  ( -15.61203582816999891, -108.4210244314312916, -5.847664976093792433 ) ) ;
#13459=CARTESIAN_POINT ( 'NONE',  ( -17.61203582817000068, -107.1622034095870077, -6.087689735156001980 ) ) ;
#13461=ADVANCED_FACE ( 'NONE', ( #2806 ), #7385, .T. ) ;
#13486=DIRECTION ( 'NONE',  ( 0.000000000000000000, 0.1872998510044689147, 0.9823027872370635460 ) ) ;
#13519=VECTOR ( 'NONE', #1748, 1000.000000000000000 ) ;
#13531=FACE_OUTER_BOUND ( 'NONE', #4467, .T. ) ;
#13586=CIRCLE ( 'NONE', #13832, 0.2000000000000012046 ) ;
#13591=DIRECTION ( 'NONE',  ( 1.000000000000000000, 1.201369187114119994E-15, 9.616040805000176517E-16 ) ) ;
#13595=ORIENTED_EDGE ( 'NONE', *, *, #3831, .F. ) ;
#13600=ORIENTED_EDGE ( 'NONE', *, *, #11394, .T. ) ;
#13606=CARTESIAN_POINT ( 'NONE',  ( -15.61203582817000068, -107.1621692949231459, -5.034900018422284518 ) ) ;
#13627=TOROIDAL_SURFACE ( 'NONE', #3360, 1.600000000000000089, 0.1499999999999999944 ) ;
#13636=AXIS2_PLACEMENT_3D ( 'NONE', #2676, #2600, #6024 ) ;
#13639=CARTESIAN_POINT ( 'NONE',  ( -15.09158957740191731, -106.8344286703292028, -4.368659857491134169 ) ) ;
#13649=ORIENTED_EDGE ( 'NONE', *, *, #11870, .T. ) ;
#13650=ORIENTED_EDGE ( 'NONE', *, *, #1503, .F. ) ;
#13661=UNCERTAINTY_MEASURE_WITH_UNIT (LENGTH_MEASURE( 1.000000000000000082E-05 ), #14710, 'distance_accuracy_value', 'NONE');
#13711=EDGE_CURVE ( 'NONE', #5900, #8946, #1068, .T. ) ;
#13745=DIRECTION ( 'NONE',  ( 0.000000000000000000, 0.1872998510044759646, 0.9823027872370621028 ) ) ;
#13822=ORIENTED_EDGE ( 'NONE', *, *, #3102, .F. ) ;
#13832=AXIS2_PLACEMENT_3D ( 'NONE', #5488, #9001, #10144 ) ;
#13836=LINE ( 'NONE', #14623, #9253 ) ;
#13841=CARTESIAN_POINT ( 'NONE',  ( -15.09158957740191731, -107.1622034095870077, -6.087689735156000204 ) ) ;
#13842=EDGE_CURVE ( 'NONE', #5903, #1553, #6562, .T. ) ;
#13850=FACE_OUTER_BOUND ( 'NONE', #9915, .T. ) ;
#13860=DIRECTION ( 'NONE',  ( 0.000000000000000000, 0.1872998510044759646, 0.9823027872370621028 ) ) ;
#13884=( NAMED_UNIT ( * ) PLANE_ANGLE_UNIT ( ) SI_UNIT ( $, .RADIAN. ) );
#13892=ORIENTED_EDGE ( 'NONE', *, *, #267, .F. ) ;
#13898=DIRECTION ( 'NONE',  ( 0.000000000000000000, 0.1872998510044759646, 0.9823027872370621028 ) ) ;
#13927=ORIENTED_EDGE ( 'NONE', *, *, #11228, .T. ) ;
#13937=DIRECTION ( 'NONE',  ( 0.000000000000000000, 0.1872998510044983078, 0.9823027872370578839 ) ) ;
#13963=ORIENTED_EDGE ( 'NONE', *, *, #6340, .T. ) ;
#13968=CARTESIAN_POINT ( 'NONE',  ( -15.61203582816999891, -106.7406604375499626, -7.297873098422156701 ) ) ;
#13987=AXIS2_PLACEMENT_3D ( 'NONE', #2514, #11764, #2594 ) ;
#14053=DIRECTION ( 'NONE',  ( -1.000000000000000000, -1.201369187114119994E-15, -9.616040805000176517E-16 ) ) ;
#14062=ORIENTED_EDGE ( 'NONE', *, *, #866, .F. ) ;
#14078=DIRECTION ( 'NONE',  ( 1.000000000000000000, 1.201369187114119994E-15, 9.616040805000176517E-16 ) ) ;
#14095=DIRECTION ( 'NONE',  ( 1.000000000000000000, 1.201369187114119994E-15, 9.616040805000176517E-16 ) ) ;
#14110=CARTESIAN_POINT ( 'NONE',  ( -15.09158957740191553, -107.4618831711941169, -7.659374194735306673 ) ) ;
#14118=ADVANCED_FACE ( 'NONE', ( #9780 ), #13163, .F. ) ;
#14143=ORIENTED_EDGE ( 'NONE', *, *, #10543, .F. ) ;
#14144=DIRECTION ( 'NONE',  ( 1.000000000000000000, 1.201369187114119994E-15, 9.616040805000176517E-16 ) ) ;
#14145=DIRECTION ( 'NONE',  ( 1.000000000000000000, 1.201369187114119994E-15, 9.616040805000176517E-16 ) ) ;
#14161=ORIENTED_EDGE ( 'NONE', *, *, #12650, .F. ) ;
#14184=DIRECTION ( 'NONE',  ( -1.000000000000000000, -1.201369187114119994E-15, -9.616040805000176517E-16 ) ) ;
#14202=CIRCLE ( 'NONE', #11747, 0.2000000000000012046 ) ;
#14204=EDGE_CURVE ( 'NONE', #10009, #11853, #13235, .T. ) ;
#14239=CARTESIAN_POINT ( 'NONE',  ( -15.61203582817000068, -106.7748397497402806, -5.108753790441425302 ) ) ;
#14243=ORIENTED_EDGE ( 'NONE', *, *, #4870, .T. ) ;
#14264=DIRECTION ( 'NONE',  ( 0.000000000000000000, -0.1872998510044521503, -0.9823027872370667657 ) ) ;
#14267=DIRECTION ( 'NONE',  ( 1.000000000000000472E-15, -0.9823027872370664326, 0.1872998510044539822 ) ) ;
#14273=ORIENTED_EDGE ( 'NONE', *, *, #2694, .T. ) ;
#14307=DIRECTION ( 'NONE',  ( 1.000000000000000000, 1.201369187114119994E-15, 9.616040805000176517E-16 ) ) ;
#14341=EDGE_CURVE ( 'NONE', #1981, #10256, #7769, .T. ) ;
#14355=EDGE_CURVE ( 'NONE', #3470, #11437, #4398, .T. ) ;
#14363=AXIS2_PLACEMENT_3D ( 'NONE', #10813, #2846, #13486 ) ;
#14425=ADVANCED_FACE ( 'NONE', ( #12761 ), #6989, .F. ) ;
#14441=ORIENTED_EDGE ( 'NONE', *, *, #12915, .T. ) ;
#14472=CIRCLE ( 'NONE', #3475, 1.249999999999999778 ) ;
#14487=EDGE_CURVE ( 'NONE', #10256, #2967, #13202, .T. ) ;
#14522=EDGE_CURVE ( 'NONE', #7227, #7782, #3722, .T. ) ;
#14557=DIRECTION ( 'NONE',  ( -1.000000000000000000, -1.201369187114119994E-15, -9.616040805000176517E-16 ) ) ;
#14569=ORIENTED_EDGE ( 'NONE', *, *, #10780, .F. ) ;
#14574=EDGE_CURVE ( 'NONE', #5848, #10870, #10739, .T. ) ;
#14576=CARTESIAN_POINT ( 'NONE',  ( -14.61203582817000246, -106.1798807882712765, -5.562105325730671623 ) ) ;
#14592=EDGE_CURVE ( 'NONE', #10777, #3470, #11829, .T. ) ;
#14600=ORIENTED_EDGE ( 'NONE', *, *, #10337, .F. ) ;
#14623=CARTESIAN_POINT ( 'NONE',  ( -15.61203582816999713, -107.9151965264422586, -6.615812085103268458 ) ) ;
#14639=ORIENTED_EDGE ( 'NONE', *, *, #11394, .F. ) ;
#14674=EDGE_CURVE ( 'NONE', #9110, #6974, #11716, .T. ) ;
#14676=VERTEX_POINT ( 'NONE', #7750 ) ;
#14700=CIRCLE ( 'NONE', #1758, 0.4500000000000011768 ) ;
#14710=( LENGTH_UNIT ( ) NAMED_UNIT ( * ) SI_UNIT ( .MILLI., .METRE. ) );
#14713=CARTESIAN_POINT ( 'NONE',  ( -14.61203582816999891, -108.0739631064533484, -6.614055049357309812 ) ) ;
#14714=AXIS2_PLACEMENT_3D ( 'NONE', #12517, #4559, #6979 ) ;
#14723=VERTEX_POINT ( 'NONE', #13361 ) ;
#14735=CARTESIAN_POINT ( 'NONE',  ( -20.61203582816999713, -107.1622034095870077, -6.087689735156005533 ) ) ;
#14737=ORIENTED_EDGE ( 'NONE', *, *, #267, .T. ) ;
#14773=EDGE_CURVE ( 'NONE', #15001, #7413, #5464, .T. ) ;
#14785=DIRECTION ( 'NONE',  ( 0.000000000000000000, 0.1872998510044689147, 0.9823027872370635460 ) ) ;
#14801=AXIS2_PLACEMENT_3D ( 'NONE', #9075, #12767, #8071 ) ;
#14805=DIRECTION ( 'NONE',  ( 0.000000000000000000, 0.1872998510044689147, 0.9823027872370635460 ) ) ;
#14806=ORIENTED_EDGE ( 'NONE', *, *, #6991, .T. ) ;
#14808=FACE_OUTER_BOUND ( 'NONE', #1984, .T. ) ;
#14891=DIRECTION ( 'NONE',  ( 0.000000000000000000, 0.1872998510044689147, 0.9823027872370635460 ) ) ;
#14950=EDGE_CURVE ( 'NONE', #10777, #6540, #3389, .T. ) ;
#14951=TOROIDAL_SURFACE ( 'NONE', #14714, 1.600000000000000089, 0.1499999999999999944 ) ;
#14957=CARTESIAN_POINT ( 'NONE',  ( -15.61203582817000246, -106.3249253597797406, -5.117531130952053253 ) ) ;
#14959=DIRECTION ( 'NONE',  ( 1.000000000000000000, 1.201369187114119994E-15, 9.616040805000176517E-16 ) ) ;
#14965=CIRCLE ( 'NONE', #4210, 0.4500000000000011768 ) ;
#14974=DIRECTION ( 'NONE',  ( 1.000000000000000000, 1.201369187114119994E-15, 9.616040805000176517E-16 ) ) ;
#15001=VERTEX_POINT ( 'NONE', #12343 ) ;
#15019=STYLED_ITEM ( 'NONE', ( #11654 ), #7461 ) ;
#15024=FILL_AREA_STYLE ('',( #2332 ) ) ;
#15025=CARTESIAN_POINT ( 'NONE',  ( -15.61203582817000068, -106.1798807882712765, -5.562105325730671623 ) ) ;
#15034=VERTEX_POINT ( 'NONE', #3076 ) ;
#15049=CIRCLE ( 'NONE', #9438, 0.2000000000000012046 ) ;
#15058=ORIENTED_EDGE ( 'NONE', *, *, #14592, .F. ) ;
#15105=ORIENTED_EDGE ( 'NONE', *, *, #531, .F. ) ;
#15118=DIRECTION ( 'NONE',  ( 0.000000000000000000, 0.1872998510044759646, 0.9823027872370621028 ) ) ;
ENDSEC;
END-ISO-10303-21;
